ISO-10303-21;
HEADER;
FILE_DESCRIPTION (('STEP AP214'),
    '1' );
FILE_NAME ('Part12^Assem2.step',
    '2026-11-01T06:29:40',
    ( '' ),
    ( '' ),
    'SwSTEP 2.0',
    'SolidWorks 2024',
    '' );
FILE_SCHEMA (( 'AUTOMOTIVE_DESIGN' ));
ENDSEC;

DATA;
#1=DIRECTION ( 'NONE',  ( -1.000000000000000000, 0.000000000000000000, 0.000000000000000000 ) ) ;
#9=CARTESIAN_POINT ( 'NONE',  ( -0.9675204218459506622, 140.4913968989433499, 501.9874629796761383 ) ) ;
#24=CARTESIAN_POINT ( 'NONE',  ( -79.99999999999995737, 146.1184945051221575, 507.7561228916242158 ) ) ;
#26=CARTESIAN_POINT ( 'NONE',  ( 0.7168072523057583689, 140.4381783004008355, 500.8620105408696759 ) ) ;
#33=SURFACE_STYLE_FILL_AREA ( #7869 ) ;
#37=DIRECTION ( 'NONE',  ( 1.450371633464475582E-15, 0.000000000000000000, 1.000000000000000000 ) ) ;
#40=EDGE_CURVE ( 'NONE', #2779, #1878, #16207, .T. ) ;
#41=ORIENTED_EDGE ( 'NONE', *, *, #2145, .F. ) ;
#47=ADVANCED_FACE ( 'NONE', ( #11337 ), #8253, .T. ) ;
#50=CARTESIAN_POINT ( 'NONE',  ( -80.02029401320167779, 140.0128597322520250, 488.8018784672104289 ) ) ;
#52=PRESENTATION_STYLE_ASSIGNMENT (( #17370 ) ) ;
#59=CARTESIAN_POINT ( 'NONE',  ( 1.000000000002633005, 138.7723821175183048, 490.5025619656410640 ) ) ;
#61=ORIENTED_EDGE ( 'NONE', *, *, #40, .F. ) ;
#65=CARTESIAN_POINT ( 'NONE',  ( -80.34799141162025649, 140.6284191703059037, 501.0624196837977138 ) ) ;
#66=COLOUR_RGB ( '', 0.40784314, 0.44705882, 0.49803922) ;
#82=COLOUR_RGB ( '', 0.40784314, 0.44705882, 0.49803922) ;
#83=DIRECTION ( 'NONE',  ( 0.000000000000000000, 0.000000000000000000, 1.000000000000000000 ) ) ;
#91=EDGE_LOOP ( 'NONE', ( #10928, #13194, #595, #9190 ) ) ;
#103=PRESENTATION_STYLE_ASSIGNMENT (( #12482 ) ) ;
#107=ORIENTED_EDGE ( 'NONE', *, *, #6001, .T. ) ;
#108=CARTESIAN_POINT ( 'NONE',  ( 1.181929469892980755, 138.7545334744432637, 496.6642397995875058 ) ) ;
#112=VECTOR ( 'NONE', #11852, 1000.000000000000000 ) ;
#113=ORIENTED_EDGE ( 'NONE', *, *, #3039, .T. ) ;
#123=CARTESIAN_POINT ( 'NONE',  ( 0.5497658814424238871, 139.8002724027203101, 500.9202994310167014 ) ) ;
#126=AXIS2_PLACEMENT_3D ( 'NONE', #3364, #17466, #11787 ) ;
#134=CIRCLE ( 'NONE', #15629, 3.883636366625808911 ) ;
#138=ADVANCED_FACE ( 'NONE', ( #10496 ), #19962, .F. ) ;
#139=ORIENTED_EDGE ( 'NONE', *, *, #1969, .T. ) ;
#147=EDGE_LOOP ( 'NONE', ( #13089, #906, #3735 ) ) ;
#162=CARTESIAN_POINT ( 'NONE',  ( -80.99999999999995737, 216.7545334744432921, 500.8237260975782874 ) ) ;
#170=ADVANCED_FACE ( 'NONE', ( #11955 ), #17305, .F. ) ;
#174=B_SPLINE_CURVE_WITH_KNOTS ( 'NONE', 3,
 ( #18997, #9526, #1676, #11279, #9328, #17269, #7796, #50, #14073, #6556 ),
 .UNSPECIFIED., .F., .F.,
 ( 4, 2, 2, 2, 4 ),
 ( 0.000000000000000000, 0.0004092867322129563616, 0.0008185734644259127233, 0.001227860196638869139, 0.001637146928851825447 ),
 .UNSPECIFIED. ) ;
#175=ORIENTED_EDGE ( 'NONE', *, *, #16048, .T. ) ;
#177=CARTESIAN_POINT ( 'NONE',  ( -79.93109621574201640, 140.7262008160015796, 502.2906755942678956 ) ) ;
#178=EDGE_LOOP ( 'NONE', ( #2107, #7086, #9051, #14398 ) ) ;
#180=AXIS2_PLACEMENT_3D ( 'NONE', #5824, #8901, #12102 ) ;
#196=EDGE_CURVE ( 'NONE', #14622, #5083, #17893, .T. ) ;
#204=SURFACE_STYLE_USAGE ( .BOTH. , #2043 ) ;
#211=CARTESIAN_POINT ( 'NONE',  ( -78.99999999999995737, 216.7545334744432921, 509.3921618609452935 ) ) ;
#215=DIRECTION ( 'NONE',  ( -1.000000000000000000, -0.000000000000000000, -0.000000000000000000 ) ) ;
#218=VECTOR ( 'NONE', #4286, 1000.000000000000000 ) ;
#222=DIRECTION ( 'NONE',  ( -5.099857904826354583E-14, -0.3949357872488052368, -0.9187087263927380398 ) ) ;
#228=DIRECTION ( 'NONE',  ( 1.000000000000000000, -0.000000000000000000, 0.000000000000000000 ) ) ;
#230=CARTESIAN_POINT ( 'NONE',  ( 0.9999999999997754019, 139.4861549369088038, 500.2186618848269859 ) ) ;
#248=EDGE_LOOP ( 'NONE', ( #19744, #15567 ) ) ;
#252=DIRECTION ( 'NONE',  ( 1.000000000000000000, 0.000000000000000000, 1.135258727068399668E-15 ) ) ;
#257=DIRECTION ( 'NONE',  ( 0.000000000000000000, 1.000000000000000000, -0.000000000000000000 ) ) ;
#263=( NAMED_UNIT ( * ) SI_UNIT ( $, .STERADIAN. ) SOLID_ANGLE_UNIT ( ) );
#305=VERTEX_POINT ( 'NONE', #6101 ) ;
#310=AXIS2_PLACEMENT_3D ( 'NONE', #19605, #3865, #10144 ) ;
#316=EDGE_LOOP ( 'NONE', ( #20231, #12649, #16992, #19805 ) ) ;
#317=EDGE_CURVE ( 'NONE', #19903, #10221, #2678, .T. ) ;
#324=EDGE_CURVE ( 'NONE', #18810, #10116, #9084, .T. ) ;
#325=CARTESIAN_POINT ( 'NONE',  ( 0.000000000000000000, 316.7545334744432353, 515.1946179577817020 ) ) ;
#329=CARTESIAN_POINT ( 'NONE',  ( -78.99999999999995737, 138.7545334744432637, 509.3921618609452935 ) ) ;
#330=DIRECTION ( 'NONE',  ( 0.000000000000000000, 1.000000000000000000, -0.000000000000000000 ) ) ;
#331=CARTESIAN_POINT ( 'NONE',  ( -64.99999999999995737, 316.7545334744432353, 495.1946179577816451 ) ) ;
#341=ORIENTED_EDGE ( 'NONE', *, *, #5552, .F. ) ;
#342=ORIENTED_EDGE ( 'NONE', *, *, #3625, .T. ) ;
#347=ORIENTED_EDGE ( 'NONE', *, *, #7611, .T. ) ;
#350=CARTESIAN_POINT ( 'NONE',  ( 0.01964375121925415052, 140.0139011465853685, 488.7997624681271418 ) ) ;
#353=( LENGTH_UNIT ( ) NAMED_UNIT ( * ) SI_UNIT ( .MILLI., .METRE. ) );
#358=DIRECTION ( 'NONE',  ( 0.000000000000000000, 0.000000000000000000, -1.000000000000000000 ) ) ;
#361=LINE ( 'NONE', #16268, #1608 ) ;
#362=ORIENTED_EDGE ( 'NONE', *, *, #20307, .T. ) ;
#368=VERTEX_POINT ( 'NONE', #3094 ) ;
#372=ORIENTED_EDGE ( 'NONE', *, *, #12021, .F. ) ;
#375=CARTESIAN_POINT ( 'NONE',  ( -3.795335389125381139E-15, 146.8256012863087960, 480.6843163258853906 ) ) ;
#377=DIRECTION ( 'NONE',  ( -1.000000000000000000, 0.000000000000000000, 1.450371633464475582E-15 ) ) ;
#392=DIRECTION ( 'NONE',  ( 0.000000000000000000, 0.000000000000000000, -1.000000000000000000 ) ) ;
#403=VECTOR ( 'NONE', #18306, 1000.000000000000000 ) ;
#410=DIRECTION ( 'NONE',  ( 0.000000000000000000, -1.000000000000000000, 0.000000000000000000 ) ) ;
#411=PRODUCT_DEFINITION_FORMATION_WITH_SPECIFIED_SOURCE ( 'ANY', '', #7599, .NOT_KNOWN. ) ;
#418=ADVANCED_FACE ( 'NONE', ( #5059 ), #7835, .T. ) ;
#435=EDGE_CURVE ( 'NONE', #10328, #18338, #2769, .T. ) ;
#438=CARTESIAN_POINT ( 'NONE',  ( -81.18192946989275072, 140.4048636633015406, 499.8237260975782874 ) ) ;
#441=DIRECTION ( 'NONE',  ( -1.000000000000000000, 0.000000000000000000, -0.000000000000000000 ) ) ;
#446=EDGE_CURVE ( 'NONE', #19368, #19036, #134, .T. ) ;
#452=CARTESIAN_POINT ( 'NONE',  ( -1.274252908074454287E-14, 140.1563709946295262, 488.5655098179835818 ) ) ;
#456=PRESENTATION_STYLE_ASSIGNMENT (( #10433 ) ) ;
#457=FACE_OUTER_BOUND ( 'NONE', #13528, .T. ) ;
#468=AXIS2_PLACEMENT_3D ( 'NONE', #18495, #1257, #15845 ) ;
#469=VERTEX_POINT ( 'NONE', #9888 ) ;
#470=VECTOR ( 'NONE', #9306, 1000.000000000000000 ) ;
#473=EDGE_CURVE ( 'NONE', #9264, #2341, #13005, .T. ) ;
#474=ORIENTED_EDGE ( 'NONE', *, *, #15207, .F. ) ;
#484=DIRECTION ( 'NONE',  ( 0.000000000000000000, -1.000000000000000000, 0.000000000000000000 ) ) ;
#497=LINE ( 'NONE', #6115, #20364 ) ;
#499=DIRECTION ( 'NONE',  ( -0.000000000000000000, -1.000000000000000000, -1.632680918566406547E-16 ) ) ;
#505=AXIS2_PLACEMENT_3D ( 'NONE', #7155, #16926, #12173 ) ;
#506=VERTEX_POINT ( 'NONE', #10189 ) ;
#507=ORIENTED_EDGE ( 'NONE', *, *, #13292, .F. ) ;
#509=VECTOR ( 'NONE', #7959, 1000.000000000000000 ) ;
#510=CARTESIAN_POINT ( 'NONE',  ( -21.85283368562565443, 317.7545334744432353, 485.1700099148404774 ) ) ;
#512=DIRECTION ( 'NONE',  ( -0.000000000000000000, 1.000000000000000000, 0.000000000000000000 ) ) ;
#517=CARTESIAN_POINT ( 'NONE',  ( 6.662140294759496685E-13, 139.7703989349477354, 490.5655098180907885 ) ) ;
#522=DIRECTION ( 'NONE',  ( 1.450371633464475779E-15, -0.000000000000000000, 1.000000000000000000 ) ) ;
#523=AXIS2_PLACEMENT_3D ( 'NONE', #2375, #835, #7149 ) ;
#526=ORIENTED_EDGE ( 'NONE', *, *, #19912, .T. ) ;
#536=MECHANICAL_DESIGN_GEOMETRIC_PRESENTATION_REPRESENTATION('',(#851),#3508);
#539=CIRCLE ( 'NONE', #19307, 0.9999999999999995559 ) ;
#543=FACE_OUTER_BOUND ( 'NONE', #6094, .T. ) ;
#565=AXIS2_PLACEMENT_3D ( 'NONE', #517, #8653, #16502 ) ;
#566=VERTEX_POINT ( 'NONE', #12354 ) ;
#567=DIRECTION ( 'NONE',  ( 0.000000000000000000, 1.179611963664227814E-13, -1.000000000000000000 ) ) ;
#578=ORIENTED_EDGE ( 'NONE', *, *, #8167, .T. ) ;
#584=VERTEX_POINT ( 'NONE', #2855 ) ;
#587=CARTESIAN_POINT ( 'NONE',  ( 1.000000000001310507, 139.7703989349544997, 489.5655098179835818 ) ) ;
#592=AXIS2_PLACEMENT_3D ( 'NONE', #9847, #2300, #6876 ) ;
#595=ORIENTED_EDGE ( 'NONE', *, *, #3023, .T. ) ;
#599=ORIENTED_EDGE ( 'NONE', *, *, #17250, .T. ) ;
#605=DIRECTION ( 'NONE',  ( 2.775557561562888827E-14, 0.000000000000000000, -1.000000000000000000 ) ) ;
#614=ORIENTED_EDGE ( 'NONE', *, *, #18375, .F. ) ;
#619=EDGE_LOOP ( 'NONE', ( #15258, #6627, #2026, #12309 ) ) ;
#622=DIRECTION ( 'NONE',  ( -1.135258727068399668E-15, 0.000000000000000000, 1.000000000000000000 ) ) ;
#625=VERTEX_POINT ( 'NONE', #4222 ) ;
#631=AXIS2_PLACEMENT_3D ( 'NONE', #7992, #9439, #17458 ) ;
#635=ORIENTED_EDGE ( 'NONE', *, *, #2291, .F. ) ;
#643=ORIENTED_EDGE ( 'NONE', *, *, #13866, .T. ) ;
#645=VERTEX_POINT ( 'NONE', #16792 ) ;
#648=ORIENTED_EDGE ( 'NONE', *, *, #12936, .T. ) ;
#649=CARTESIAN_POINT ( 'NONE',  ( -1.000000000000004885, 146.1184945051221860, 507.7561228916242158 ) ) ;
#652=CIRCLE ( 'NONE', #15493, 9.000000000000007105 ) ;
#661=CARTESIAN_POINT ( 'NONE',  ( 0.000000000000000000, 216.7545334744432921, 155.1946179577816167 ) ) ;
#667=EDGE_CURVE ( 'NONE', #1728, #12429, #6413, .T. ) ;
#679=CARTESIAN_POINT ( 'NONE',  ( 0.3266166635162791043, 138.8954520623098006, 489.3238097202654444 ) ) ;
#689=EDGE_CURVE ( 'NONE', #17495, #15985, #20159, .T. ) ;
#704=CARTESIAN_POINT ( 'NONE',  ( -80.02433601516246142, 140.0032791352475101, 488.8200091561060958 ) ) ;
#740=EDGE_LOOP ( 'NONE', ( #19768, #8935, #9607, #17560 ) ) ;
#751=DIRECTION ( 'NONE',  ( 1.000000000000000000, 0.000000000000000000, 0.000000000000000000 ) ) ;
#755=DIRECTION ( 'NONE',  ( 0.000000000000000000, -1.632680918566406547E-16, 1.000000000000000000 ) ) ;
#761=ORIENTED_EDGE ( 'NONE', *, *, #14778, .T. ) ;
#763=ORIENTED_EDGE ( 'NONE', *, *, #17421, .F. ) ;
#766=CIRCLE ( 'NONE', #5404, 3.883636366625808911 ) ;
#769=ORIENTED_EDGE ( 'NONE', *, *, #17561, .T. ) ;
#771=EDGE_LOOP ( 'NONE', ( #8188, #13263, #7189, #7082 ) ) ;
#778=CARTESIAN_POINT ( 'NONE',  ( 0.05191788718346542625, 139.0018976549732201, 488.9266887137286517 ) ) ;
#784=FACE_OUTER_BOUND ( 'NONE', #12554, .T. ) ;
#786=DIRECTION ( 'NONE',  ( 0.000000000000000000, 0.000000000000000000, 1.000000000000000000 ) ) ;
#792=VERTEX_POINT ( 'NONE', #6275 ) ;
#817=CARTESIAN_POINT ( 'NONE',  ( 0.000000000000000000, 141.3905724437643698, 484.7051316060566819 ) ) ;
#821=LINE ( 'NONE', #10201, #470 ) ;
#829=ORIENTED_EDGE ( 'NONE', *, *, #689, .F. ) ;
#833=UNCERTAINTY_MEASURE_WITH_UNIT (LENGTH_MEASURE( 1.000000000000000082E-05 ), #11594, 'distance_accuracy_value', 'NONE');
#835=DIRECTION ( 'NONE',  ( -1.322948291343119651E-12, 0.000000000000000000, 1.000000000000000000 ) ) ;
#851=STYLED_ITEM ( 'NONE', ( #18019 ), #2851 ) ;
#866=CIRCLE ( 'NONE', #6480, 9.000000000000007105 ) ;
#875=CARTESIAN_POINT ( 'NONE',  ( 1.000000000001388889, 138.8314847490560169, 489.5655098179835818 ) ) ;
#876=EDGE_CURVE ( 'NONE', #19179, #305, #7095, .T. ) ;
#890=EDGE_CURVE ( 'NONE', #13927, #19179, #16314, .T. ) ;
#891=DIRECTION ( 'NONE',  ( -1.132388935707081510E-15, 0.000000000000000000, 1.000000000000000000 ) ) ;
#896=CARTESIAN_POINT ( 'NONE',  ( -79.99999999999995737, 142.0976792249508946, 485.4122383872432351 ) ) ;
#906=ORIENTED_EDGE ( 'NONE', *, *, #9151, .T. ) ;
#918=CARTESIAN_POINT ( 'NONE',  ( -58.16843972078500258, 319.7545334744432353, 485.1700099148404206 ) ) ;
#921=CARTESIAN_POINT ( 'NONE',  ( -80.73513083854561501, 138.7723821183164148, 490.5025619529872642 ) ) ;
#931=AXIS2_PLACEMENT_3D ( 'NONE', #2693, #16741, #2591 ) ;
#932=VECTOR ( 'NONE', #17872, 1000.000000000000000 ) ;
#940=CYLINDRICAL_SURFACE ( 'NONE', #16966, 1.000000000000000888 ) ;
#952=ORIENTED_EDGE ( 'NONE', *, *, #15897, .F. ) ;
#957=DIRECTION ( 'NONE',  ( -1.000000000000000000, -0.000000000000000000, -1.135258727068399668E-15 ) ) ;
#959=ORIENTED_EDGE ( 'NONE', *, *, #2434, .F. ) ;
#962=LINE ( 'NONE', #7292, #8627 ) ;
#968=DIRECTION ( 'NONE',  ( 0.000000000000000000, -1.000000000000000000, 0.000000000000000000 ) ) ;
#971=ORIENTED_EDGE ( 'NONE', *, *, #3266, .F. ) ;
#978=EDGE_CURVE ( 'NONE', #19144, #11820, #1160, .T. ) ;
#979=CIRCLE ( 'NONE', #13853, 1.000000000000015987 ) ;
#985=CIRCLE ( 'NONE', #10894, 1.000000000000000888 ) ;
#989=FACE_OUTER_BOUND ( 'NONE', #20233, .T. ) ;
#996=AXIS2_PLACEMENT_3D ( 'NONE', #2680, #13520, #9273 ) ;
#999=ORIENTED_EDGE ( 'NONE', *, *, #2461, .F. ) ;
#1010=SURFACE_SIDE_STYLE ('',( #4041 ) ) ;
#1016=ORIENTED_EDGE ( 'NONE', *, *, #6617, .F. ) ;
#1021=VERTEX_POINT ( 'NONE', #2533 ) ;
#1032=CARTESIAN_POINT ( 'NONE',  ( 3.215259230344088024E-13, 140.4048636633015406, 499.8237260975782874 ) ) ;
#1036=EDGE_CURVE ( 'NONE', #12344, #4262, #4496, .T. ) ;
#1045=ORIENTED_EDGE ( 'NONE', *, *, #16350, .T. ) ;
#1046=CARTESIAN_POINT ( 'NONE',  ( -41.50085094405407915, 175.4489062796178871, 505.3921618609452935 ) ) ;
#1051=VECTOR ( 'NONE', #10624, 1000.000000000000000 ) ;
#1071=CARTESIAN_POINT ( 'NONE',  ( -81.18192946989245229, 138.7545334744432637, 491.0690926367356042 ) ) ;
#1082=LINE ( 'NONE', #7417, #17652 ) ;
#1090=AXIS2_PLACEMENT_3D ( 'NONE', #7561, #20225, #18161 ) ;
#1121=CARTESIAN_POINT ( 'NONE',  ( -38.50085094405407204, 159.0821755739672483, 505.3921618609452935 ) ) ;
#1122=CARTESIAN_POINT ( 'NONE',  ( -80.85993302188293796, 138.8314847507810725, 489.5655098117073862 ) ) ;
#1132=EDGE_CURVE ( 'NONE', #566, #3836, #6778, .T. ) ;
#1134=CARTESIAN_POINT ( 'NONE',  ( 1.181929469892549323, 139.7545334744432637, 491.0690926367356042 ) ) ;
#1137=CARTESIAN_POINT ( 'NONE',  ( -79.63624027127092120, 139.7550675453751694, 500.7965084021044504 ) ) ;
#1142=ORIENTED_EDGE ( 'NONE', *, *, #9857, .F. ) ;
#1145=VERTEX_POINT ( 'NONE', #15640 ) ;
#1155=DIRECTION ( 'NONE',  ( 0.000000000000000000, -0.7071067811865494601, 0.7071067811865456854 ) ) ;
#1160=LINE ( 'NONE', #6041, #1791 ) ;
#1161=( NAMED_UNIT ( * ) PLANE_ANGLE_UNIT ( ) SI_UNIT ( $, .RADIAN. ) );
#1171=STYLED_ITEM ( 'NONE', ( #13407 ), #9595 ) ;
#1176=CARTESIAN_POINT ( 'NONE',  ( 1.181929469891187301, 216.7545334744432921, 489.5655098179833544 ) ) ;
#1178=ORIENTED_EDGE ( 'NONE', *, *, #11437, .F. ) ;
#1188=DIRECTION ( 'NONE',  ( -0.000000000000000000, 1.000000000000000000, 1.632680918566406547E-16 ) ) ;
#1190=SURFACE_STYLE_USAGE ( .BOTH. , #18419 ) ;
#1196=AXIS2_PLACEMENT_3D ( 'NONE', #211, #6615, #13119 ) ;
#1205=CARTESIAN_POINT ( 'NONE',  ( -79.99999999999995737, 152.4824555358011082, 486.3411705753778165 ) ) ;
#1208=UNCERTAINTY_MEASURE_WITH_UNIT (LENGTH_MEASURE( 1.000000000000000082E-05 ), #12422, 'distance_accuracy_value', 'NONE');
#1215=FILL_AREA_STYLE ('',( #3306 ) ) ;
#1220=EDGE_LOOP ( 'NONE', ( #20096, #14071, #18783, #7511 ) ) ;
#1231=DIRECTION ( 'NONE',  ( 1.000000000000000000, -0.000000000000000000, 0.000000000000000000 ) ) ;
#1241=ORIENTED_EDGE ( 'NONE', *, *, #4726, .T. ) ;
#1242=( BOUNDED_SURFACE ( )  B_SPLINE_SURFACE ( 3, 2, ( 
 ( #3172, #15860, #14189 ),
 ( #17694, #177, #3373 ),
 ( #6577, #9453, #4714 ),
 ( #15762, #8325, #12869 ),
 ( #8219, #17478, #12549 ),
 ( #17591, #1590, #7910 ),
 ( #16177, #11005, #12659 ),
 ( #6273, #9652, #6374 ),
 ( #65, #18925, #2005 ),
 ( #20361, #19126, #4828 ),
 ( #15979, #11102, #17288 ),
 ( #17384, #1819, #4920 ),
 ( #3269, #3583, #14494 ),
 ( #11200, #6474, #18812 ) ),
 .UNSPECIFIED., .F., .F., .T. ) 
 B_SPLINE_SURFACE_WITH_KNOTS ( ( 4, 2, 2, 2, 2, 2, 4 ),
 ( 3, 3 ),
 ( 0.001011094481076133932, 0.001870411825472422613, 0.002300070497670567062, 0.002729729169868711294, 0.003159387842066855526, 0.003589046514264999758, 0.004448363858661288223 ),
 ( 0.000000000000000000, 1.000000000000000000 ),
 .UNSPECIFIED. ) 
 GEOMETRIC_REPRESENTATION_ITEM ( )  RATIONAL_B_SPLINE_SURFACE ( (
 ( 1.000000000000000000, 0.7071067811865475727, 1.000000000000000000),
 ( 1.000000000000000000, 0.7323290926429416592, 1.000000000000000000),
 ( 1.000000000000000000, 0.7535416720974540405, 1.000000000000000000),
 ( 1.000000000000000000, 0.7799492680867576855, 1.000000000000000000),
 ( 1.000000000000000000, 0.7878446813477756328, 1.000000000000000000),
 ( 1.000000000000000000, 0.8013484601504040628, 1.000000000000000000),
 ( 1.000000000000000000, 0.8070584780280735115, 1.000000000000000000),
 ( 1.000000000000000000, 0.8167183804147478687, 1.000000000000000000),
 ( 1.000000000000000000, 0.8205285662994377116, 1.000000000000000000),
 ( 1.000000000000000000, 0.8265885805974317879, 1.000000000000000000),
 ( 1.000000000000000000, 0.8288784836241653853, 1.000000000000000000),
 ( 1.000000000000000000, 0.8339575989303936732, 1.000000000000000000),
 ( 1.000000000000000000, 0.8350775064303027628, 1.000000000000000000),
 ( 1.000000000000000000, 0.8351454326190045352, 1.000000000000000000) ) ) 
 REPRESENTATION_ITEM ( '' )  SURFACE ( )  );
#1253=DIRECTION ( 'NONE',  ( 1.000000000000000000, -0.000000000000000000, -0.000000000000000000 ) ) ;
#1255=DIRECTION ( 'NONE',  ( 0.000000000000000000, 0.000000000000000000, -1.000000000000000000 ) ) ;
#1257=DIRECTION ( 'NONE',  ( -0.000000000000000000, -1.000000000000000000, -0.000000000000000000 ) ) ;
#1260=DIRECTION ( 'NONE',  ( 0.000000000000000000, 0.000000000000000000, 1.000000000000000000 ) ) ;
#1283=( NAMED_UNIT ( * ) SI_UNIT ( $, .STERADIAN. ) SOLID_ANGLE_UNIT ( ) );
#1285=DIRECTION ( 'NONE',  ( -0.000000000000000000, -0.000000000000000000, 1.000000000000000000 ) ) ;
#1287=EDGE_CURVE ( 'NONE', #14622, #18716, #6528, .T. ) ;
#1295=EDGE_CURVE ( 'NONE', #2815, #14814, #12637, .T. ) ;
#1298=FILL_AREA_STYLE_COLOUR ( '', #7408 ) ;
#1310=LINE ( 'NONE', #4864, #6423 ) ;
#1316=ADVANCED_FACE ( 'NONE', ( #19694 ), #14623, .T. ) ;
#1317=COLOUR_RGB ( '', 0.40784314, 0.44705882, 0.49803922) ;
#1323=FACE_OUTER_BOUND ( 'NONE', #3933, .T. ) ;
#1324=ORIENTED_EDGE ( 'NONE', *, *, #15595, .T. ) ;
#1332=DIRECTION ( 'NONE',  ( 0.000000000000000000, 0.000000000000000000, -1.000000000000000000 ) ) ;
#1335=FACE_OUTER_BOUND ( 'NONE', #3758, .T. ) ;
#1342=FILL_AREA_STYLE_COLOUR ( '', #1700 ) ;
#1351=CARTESIAN_POINT ( 'NONE',  ( 0.07056292634023825228, 141.0639970544592927, 501.4403512417491129 ) ) ;
#1394=FACE_OUTER_BOUND ( 'NONE', #17894, .T. ) ;
#1410=ORIENTED_EDGE ( 'NONE', *, *, #3355, .T. ) ;
#1414=VECTOR ( 'NONE', #16185, 1000.000000000000000 ) ;
#1425=MECHANICAL_DESIGN_GEOMETRIC_PRESENTATION_REPRESENTATION('',(#2429),#6064);
#1433=CARTESIAN_POINT ( 'NONE',  ( -64.99999999999995737, 316.7545334744432353, 495.1946179577816451 ) ) ;
#1439=STYLED_ITEM ( 'NONE', ( #18650 ), #1705 ) ;
#1449=CARTESIAN_POINT ( 'NONE',  ( -81.18192946989275072, 140.4048636633015406, 499.8237260975782874 ) ) ;
#1456=CARTESIAN_POINT ( 'NONE',  ( 0.3890055088326604404, 139.8536359628922128, 501.0133158358985384 ) ) ;
#1458=CIRCLE ( 'NONE', #9386, 1.000000000000004219 ) ;
#1465=VERTEX_POINT ( 'NONE', #8477 ) ;
#1467=DIRECTION ( 'NONE',  ( 0.000000000000000000, -0.000000000000000000, 1.000000000000000000 ) ) ;
#1472=VECTOR ( 'NONE', #2062, 1000.000000000000000 ) ;
#1482=VERTEX_POINT ( 'NONE', #10024 ) ;
#1490=CARTESIAN_POINT ( 'NONE',  ( 1.000000000002633005, 139.7703989349544145, 490.5655098179835818 ) ) ;
#1494=CIRCLE ( 'NONE', #13066, 3.000000000000002665 ) ;
#1517=VERTEX_POINT ( 'NONE', #6747 ) ;
#1518=EDGE_LOOP ( 'NONE', ( #17202, #12283, #16460, #635 ) ) ;
#1519=EDGE_LOOP ( 'NONE', ( #14022, #14032, #2450, #15611 ) ) ;
#1523=DIRECTION ( 'NONE',  ( 3.925231146709346286E-14, -0.7071067811865614505, 0.7071067811865336949 ) ) ;
#1524=PRESENTATION_STYLE_ASSIGNMENT (( #7743 ) ) ;
#1533=SURFACE_STYLE_FILL_AREA ( #1215 ) ;
#1536=DIRECTION ( 'NONE',  ( 0.000000000000000000, 0.000000000000000000, -1.000000000000000000 ) ) ;
#1537=EDGE_CURVE ( 'NONE', #19958, #8826, #16425, .T. ) ;
#1550=CARTESIAN_POINT ( 'NONE',  ( 0.8548291518614077322, 139.4861549401841785, 500.2186618924462209 ) ) ;
#1558=FACE_OUTER_BOUND ( 'NONE', #16436, .T. ) ;
#1564=ORIENTED_EDGE ( 'NONE', *, *, #15818, .T. ) ;
#1573=DIRECTION ( 'NONE',  ( 3.328238341717372086E-14, 0.000000000000000000, -1.000000000000000000 ) ) ;
#1580=DIRECTION ( 'NONE',  ( -1.000000000000000000, -0.000000000000000000, -1.135258727068399668E-15 ) ) ;
#1587=ORIENTED_EDGE ( 'NONE', *, *, #19459, .F. ) ;
#1589=ORIENTED_EDGE ( 'NONE', *, *, #8146, .F. ) ;
#1590=CARTESIAN_POINT ( 'NONE',  ( -79.98592531253316906, 140.1739456240907771, 501.5312821746164218 ) ) ;
#1591=VERTEX_POINT ( 'NONE', #8677 ) ;
#1594=CIRCLE ( 'NONE', #19033, 1.000000000000000888 ) ;
#1599=DIRECTION ( 'NONE',  ( -0.000000000000000000, -0.000000000000000000, -1.000000000000000000 ) ) ;
#1606=FACE_OUTER_BOUND ( 'NONE', #13424, .T. ) ;
#1608=VECTOR ( 'NONE', #11407, 1000.000000000000000 ) ;
#1610=CARTESIAN_POINT ( 'NONE',  ( 0.000000000000000000, 0.000000000000000000, 0.000000000000000000 ) ) ;
#1615=ORIENTED_EDGE ( 'NONE', *, *, #4504, .F. ) ;
#1619=FILL_AREA_STYLE ('',( #3202 ) ) ;
#1630=CARTESIAN_POINT ( 'NONE',  ( -79.99999999999995737, 152.4824555358011082, 486.3411705753778165 ) ) ;
#1631=LINE ( 'NONE', #14344, #9700 ) ;
#1632=VECTOR ( 'NONE', #2614, 1000.000000000000000 ) ;
#1635=EDGE_CURVE ( 'NONE', #10821, #2527, #3114, .T. ) ;
#1638=ADVANCED_FACE ( 'NONE', ( #8874 ), #6084, .T. ) ;
#1639=ORIENTED_EDGE ( 'NONE', *, *, #7611, .F. ) ;
#1642=EDGE_LOOP ( 'NONE', ( #2207, #13694, #5259, #19708 ) ) ;
#1648=CARTESIAN_POINT ( 'NONE',  ( -0.6579963148074815527, 139.9810361770940688, 501.2022436020878899 ) ) ;
#1676=CARTESIAN_POINT ( 'NONE',  ( -80.72548054392764527, 139.7734801347532994, 489.5367579066505073 ) ) ;
#1680=DIRECTION ( 'NONE',  ( 8.479266908829339085E-16, -1.000000000000000000, 0.000000000000000000 ) ) ;
#1682=EDGE_CURVE ( 'NONE', #8340, #19125, #14211, .T. ) ;
#1683=DIRECTION ( 'NONE',  ( 0.000000000000000000, -1.000000000000000000, 0.000000000000000000 ) ) ;
#1685=DIRECTION ( 'NONE',  ( -1.000000000000000000, 0.000000000000000000, 0.000000000000000000 ) ) ;
#1691=CIRCLE ( 'NONE', #14873, 1.000000000000000888 ) ;
#1700=COLOUR_RGB ( '', 0.09019608, 0.27058824, 0.51372549) ;
#1705=ADVANCED_FACE ( 'NONE', ( #10612, #13805, #5978 ), #18837, .F. ) ;
#1728=VERTEX_POINT ( 'NONE', #5053 ) ;
#1733=VECTOR ( 'NONE', #2376, 1000.000000000000000 ) ;
#1742=AXIS2_PLACEMENT_3D ( 'NONE', #15046, #4132, #4010 ) ;
#1747=VECTOR ( 'NONE', #15870, 1000.000000000000000 ) ;
#1754=ORIENTED_EDGE ( 'NONE', *, *, #7794, .F. ) ;
#1758=CYLINDRICAL_SURFACE ( 'NONE', #9054, 1.000000000000015987 ) ;
#1761=CARTESIAN_POINT ( 'NONE',  ( 0.04009716062711748963, 139.6070811926061879, 500.4884095045860590 ) ) ;
#1763=CARTESIAN_POINT ( 'NONE',  ( 1.000000000002633005, 138.7723821175183048, 490.5025619656410640 ) ) ;
#1766=CARTESIAN_POINT ( 'NONE',  ( 0.000000000000000000, 216.7545334744432921, 515.1946179577817020 ) ) ;
#1774=EDGE_LOOP ( 'NONE', ( #6198, #2231, #6097, #2830 ) ) ;
#1775=DIRECTION ( 'NONE',  ( 1.000000000000000000, 0.000000000000000000, 3.328238341717372086E-14 ) ) ;
#1779=ORIENTED_EDGE ( 'NONE', *, *, #9646, .T. ) ;
#1789=ORIENTED_EDGE ( 'NONE', *, *, #11501, .F. ) ;
#1790=DIRECTION ( 'NONE',  ( 0.000000000000000000, 1.000000000000000000, 0.000000000000000000 ) ) ;
#1791=VECTOR ( 'NONE', #10571, 1000.000000000000000 ) ;
#1799=ORIENTED_EDGE ( 'NONE', *, *, #15038, .F. ) ;
#1806=CARTESIAN_POINT ( 'NONE',  ( 1.181929469893224560, 216.7545334744432921, 499.8237260975781737 ) ) ;
#1809=CARTESIAN_POINT ( 'NONE',  ( -0.9575141835544629387, 139.0431362428743682, 488.7923103725937040 ) ) ;
#1812=EDGE_CURVE ( 'NONE', #14622, #11075, #10014, .T. ) ;
#1819=CARTESIAN_POINT ( 'NONE',  ( -80.63015381190217568, 139.7734858225249752, 500.8736181254813573 ) ) ;
#1820=ORIENTED_EDGE ( 'NONE', *, *, #14720, .T. ) ;
#1844=CARTESIAN_POINT ( 'NONE',  ( -1.301042606982605321E-14, 152.4824555358010798, 501.3921618609452366 ) ) ;
#1852=EDGE_CURVE ( 'NONE', #17380, #13927, #1458, .T. ) ;
#1853=CARTESIAN_POINT ( 'NONE',  ( -82.18192946989277914, 216.7545334744432921, 500.8237260975782874 ) ) ;
#1862=PLANE ( 'NONE',  #12048 ) ;
#1864=CARTESIAN_POINT ( 'NONE',  ( -1.000000000000012212, 140.8764026050585301, 502.4686618848270996 ) ) ;
#1878=VERTEX_POINT ( 'NONE', #3835 ) ;
#1883=DIRECTION ( 'NONE',  ( 0.000000000000000000, 0.000000000000000000, 1.000000000000000000 ) ) ;
#1888=CARTESIAN_POINT ( 'NONE',  ( -64.99999999999995737, 317.7545334744432353, 475.1454018718993098 ) ) ;
#1905=EDGE_LOOP ( 'NONE', ( #1016, #10973, #19641, #10313 ) ) ;
#1911=CARTESIAN_POINT ( 'NONE',  ( 1.181929469893224560, 138.7545334744432637, 499.8237260975781737 ) ) ;
#1912=FACE_OUTER_BOUND ( 'NONE', #5078, .T. ) ;
#1917=CARTESIAN_POINT ( 'NONE',  ( -82.18192946989243808, 139.7703989349477354, 490.5655098180907316 ) ) ;
#1924=ORIENTED_EDGE ( 'NONE', *, *, #12318, .F. ) ;
#1925=EDGE_CURVE ( 'NONE', #6397, #12344, #19262, .T. ) ;
#1950=CARTESIAN_POINT ( 'NONE',  ( 1.181929469893224560, 140.4048636633015406, 499.8237260975782874 ) ) ;
#1963=DIRECTION ( 'NONE',  ( 0.000000000000000000, 0.000000000000000000, -1.000000000000000000 ) ) ;
#1969=EDGE_CURVE ( 'NONE', #10840, #17862, #17940, .T. ) ;
#1971=AXIS2_PLACEMENT_3D ( 'NONE', #11156, #15511, #1332 ) ;
#1972=VECTOR ( 'NONE', #7634, 1000.000000000000000 ) ;
#1974=ORIENTED_EDGE ( 'NONE', *, *, #10232, .T. ) ;
#1982=EDGE_LOOP ( 'NONE', ( #11263, #10070, #7892, #18376 ) ) ;
#1986=SURFACE_STYLE_FILL_AREA ( #15166 ) ;
#1987=PLANE ( 'NONE',  #10703 ) ;
#1992=DIRECTION ( 'NONE',  ( -1.000000000000000000, -0.000000000000000000, -0.000000000000000000 ) ) ;
#1997=FACE_OUTER_BOUND ( 'NONE', #316, .T. ) ;
#2005=CARTESIAN_POINT ( 'NONE',  ( -79.69598282171878623, 139.7376548800553167, 500.7557224526424307 ) ) ;
#2013=CARTESIAN_POINT ( 'NONE',  ( -81.18192946989275072, 138.7545334744432637, 499.8237260975782874 ) ) ;
#2014=DIRECTION ( 'NONE',  ( 0.000000000000000000, 1.000000000000000000, 0.000000000000000000 ) ) ;
#2022=VERTEX_POINT ( 'NONE', #10179 ) ;
#2026=ORIENTED_EDGE ( 'NONE', *, *, #18842, .T. ) ;
#2041=CARTESIAN_POINT ( 'NONE',  ( 1.181929469892510243, 139.7703989349544145, 489.5655098179833544 ) ) ;
#2043=SURFACE_SIDE_STYLE ('',( #6500 ) ) ;
#2044=COLOUR_RGB ( '', 0.08235294, 0.09019608, 0.10196078) ;
#2051=AXIS2_PLACEMENT_3D ( 'NONE', #17748, #2174, #8478 ) ;
#2052=AXIS2_PLACEMENT_3D ( 'NONE', #17164, #1580, #20350 ) ;
#2054=AXIS2_PLACEMENT_3D ( 'NONE', #7912, #6377, #15765 ) ;
#2057=ADVANCED_FACE ( 'NONE', ( #8121 ), #2275, .T. ) ;
#2062=DIRECTION ( 'NONE',  ( -0.000000000000000000, -1.000000000000000000, -0.000000000000000000 ) ) ;
#2065=CLOSED_SHELL ( 'NONE', ( #3585, #13041, #2334, #5565, #16861, #8508, #7526 ) ) ;
#2066=AXIS2_PLACEMENT_3D ( 'NONE', #20280, #1285, #8947 ) ;
#2087=UNCERTAINTY_MEASURE_WITH_UNIT (LENGTH_MEASURE( 1.000000000000000082E-05 ), #20169, 'distance_accuracy_value', 'NONE');
#2100=COLOUR_RGB ( '', 0.31764706, 0.68627451, 0.89019608) ;
#2101=ORIENTED_EDGE ( 'NONE', *, *, #6169, .T. ) ;
#2107=ORIENTED_EDGE ( 'NONE', *, *, #5273, .T. ) ;
#2116=AXIS2_PLACEMENT_3D ( 'NONE', #10322, #5799, #7150 ) ;
#2123=FILL_AREA_STYLE ('',( #17697 ) ) ;
#2129=CARTESIAN_POINT ( 'NONE',  ( -0.6025106023757541562, 138.8732404265368814, 489.6068043582602627 ) ) ;
#2131=LINE ( 'NONE', #375, #12985 ) ;
#2144=CIRCLE ( 'NONE', #1090, 1.000000000000000888 ) ;
#2145=EDGE_CURVE ( 'NONE', #19958, #469, #16970, .T. ) ;
#2148=DIRECTION ( 'NONE',  ( -0.000000000000000000, -1.000000000000000000, -0.000000000000000000 ) ) ;
#2149=CIRCLE ( 'NONE', #8078, 3.000000000000016431 ) ;
#2158=EDGE_CURVE ( 'NONE', #9243, #16969, #2149, .T. ) ;
#2159=CARTESIAN_POINT ( 'NONE',  ( -79.99999999999995737, 316.7545334744432353, 515.1946179577817020 ) ) ;
#2168=LINE ( 'NONE', #11562, #13633 ) ;
#2173=AXIS2_PLACEMENT_3D ( 'NONE', #16496, #11541, #4130 ) ;
#2174=DIRECTION ( 'NONE',  ( 0.000000000000000000, -0.7071067811865336949, 0.7071067811865614505 ) ) ;
#2207=ORIENTED_EDGE ( 'NONE', *, *, #7625, .F. ) ;
#2216=VERTEX_POINT ( 'NONE', #9593 ) ;
#2218=ORIENTED_EDGE ( 'NONE', *, *, #13696, .T. ) ;
#2221=CARTESIAN_POINT ( 'NONE',  ( 0.02255891082085830293, 139.0238496639661037, 488.8482061044569491 ) ) ;
#2231=ORIENTED_EDGE ( 'NONE', *, *, #3266, .T. ) ;
#2235=CARTESIAN_POINT ( 'NONE',  ( -78.99999999999997158, 139.1621397082989233, 488.3874972750760435 ) ) ;
#2237=CARTESIAN_POINT ( 'NONE',  ( -79.99999999999995737, 138.7545334744432637, 478.3411705753777596 ) ) ;
#2240=FILL_AREA_STYLE_COLOUR ( '', #7739 ) ;
#2243=CARTESIAN_POINT ( 'NONE',  ( 0.000000000000000000, 316.7545334744432921, 205.1946179577815883 ) ) ;
#2270=DIRECTION ( 'NONE',  ( -0.000000000000000000, -1.000000000000000000, -1.632680918566406547E-16 ) ) ;
#2274=ADVANCED_FACE ( 'NONE', ( #14354 ), #3433, .F. ) ;
#2275=PLANE ( 'NONE',  #7439 ) ;
#2283=EDGE_CURVE ( 'NONE', #12201, #9147, #14662, .T. ) ;
#2291=EDGE_CURVE ( 'NONE', #8271, #16331, #14243, .T. ) ;
#2300=DIRECTION ( 'NONE',  ( 0.000000000000000000, 1.000000000000000000, 0.000000000000000000 ) ) ;
#2301=DIRECTION ( 'NONE',  ( 0.000000000000000000, 1.632680918566406793E-16, -1.000000000000000000 ) ) ;
#2315=DIRECTION ( 'NONE',  ( 0.000000000000000000, -1.000000000000000000, 0.000000000000000000 ) ) ;
#2320=( LENGTH_UNIT ( ) NAMED_UNIT ( * ) SI_UNIT ( .MILLI., .METRE. ) );
#2321=VECTOR ( 'NONE', #3722, 1000.000000000000114 ) ;
#2322=EDGE_CURVE ( 'NONE', #5003, #17127, #16031, .T. ) ;
#2325=CARTESIAN_POINT ( 'NONE',  ( 0.8686015887051632411, 139.7703989352353346, 489.5655098179837523 ) ) ;
#2329=AXIS2_PLACEMENT_3D ( 'NONE', #18828, #8029, #12781 ) ;
#2334=ADVANCED_FACE ( 'NONE', ( #3319 ), #1862, .F. ) ;
#2341=VERTEX_POINT ( 'NONE', #5085 ) ;
#2343=( LENGTH_UNIT ( ) NAMED_UNIT ( * ) SI_UNIT ( .MILLI., .METRE. ) );
#2352=CYLINDRICAL_SURFACE ( 'NONE', #2173, 1.000000000000000888 ) ;
#2355=CARTESIAN_POINT ( 'NONE',  ( 0.9999999999998859801, 140.4048636633015406, 500.8237260975781737 ) ) ;
#2362=VERTEX_POINT ( 'NONE', #16635 ) ;
#2372=VECTOR ( 'NONE', #5639, 1000.000000000000000 ) ;
#2374=EDGE_LOOP ( 'NONE', ( #9766, #15777, #1639, #9611 ) ) ;
#2375=CARTESIAN_POINT ( 'NONE',  ( -82.18192946989240966, 138.7545334744432637, 489.5655098179820470 ) ) ;
#2376=DIRECTION ( 'NONE',  ( -1.000000000000000000, -0.000000000000000000, 1.017652531801993019E-13 ) ) ;
#2381=MECHANICAL_DESIGN_GEOMETRIC_PRESENTATION_REPRESENTATION('',(#9974),#17517);
#2398=CARTESIAN_POINT ( 'NONE',  ( -79.31189707736970718, 140.0116299656163505, 501.2541794163659574 ) ) ;
#2404=FACE_OUTER_BOUND ( 'NONE', #1774, .T. ) ;
#2409=CARTESIAN_POINT ( 'NONE',  ( -44.50085094405407915, 159.0821755739672483, 510.3921618609452935 ) ) ;
#2415=ORIENTED_EDGE ( 'NONE', *, *, #13797, .F. ) ;
#2421=ORIENTED_EDGE ( 'NONE', *, *, #3726, .T. ) ;
#2429=STYLED_ITEM ( 'NONE', ( #3515 ), #418 ) ;
#2432=CARTESIAN_POINT ( 'NONE',  ( 0.7188359785814644187, 138.8395712689028301, 489.5362691342353401 ) ) ;
#2433=FILL_AREA_STYLE_COLOUR ( '', #7715 ) ;
#2434=EDGE_CURVE ( 'NONE', #6152, #2022, #14019, .T. ) ;
#2435=DIRECTION ( 'NONE',  ( 0.000000000000000000, 0.000000000000000000, 1.000000000000000000 ) ) ;
#2436=MECHANICAL_DESIGN_GEOMETRIC_PRESENTATION_REPRESENTATION('',(#16304),#9360);
#2448=VECTOR ( 'NONE', #3586, 1000.000000000000000 ) ;
#2450=ORIENTED_EDGE ( 'NONE', *, *, #2283, .F. ) ;
#2455=CIRCLE ( 'NONE', #1971, 1.000000000000000888 ) ;
#2456=FILL_AREA_STYLE ('',( #9991 ) ) ;
#2461=EDGE_CURVE ( 'NONE', #17380, #19144, #4820, .T. ) ;
#2464=PLANE ( 'NONE',  #15705 ) ;
#2470=ADVANCED_FACE ( 'NONE', ( #18037 ), #3935, .F. ) ;
#2475=CIRCLE ( 'NONE', #12352, 9.000000000000007105 ) ;
#2476=ADVANCED_FACE ( 'NONE', ( #11875 ), #8094, .T. ) ;
#2479=ORIENTED_EDGE ( 'NONE', *, *, #11758, .T. ) ;
#2487=APPLICATION_CONTEXT ( 'automotive_design' ) ;
#2489=DIRECTION ( 'NONE',  ( 3.328238341717372086E-14, 0.000000000000000000, -1.000000000000000000 ) ) ;
#2509=UNCERTAINTY_MEASURE_WITH_UNIT (LENGTH_MEASURE( 1.000000000000000082E-05 ), #4318, 'distance_accuracy_value', 'NONE');
#2513=DIRECTION ( 'NONE',  ( -1.000000000000000000, -0.000000000000000000, -0.000000000000000000 ) ) ;
#2526=ORIENTED_EDGE ( 'NONE', *, *, #12912, .T. ) ;
#2527=VERTEX_POINT ( 'NONE', #14030 ) ;
#2530=CARTESIAN_POINT ( 'NONE',  ( 0.000000000000000000, 216.7545334744432921, 0.000000000000000000 ) ) ;
#2532=EDGE_LOOP ( 'NONE', ( #19110, #13908, #5128, #12475, #5947, #4332 ) ) ;
#2533=CARTESIAN_POINT ( 'NONE',  ( 1.181929469892950335, 138.7545334744432637, 496.6642397995874489 ) ) ;
#2536=CARTESIAN_POINT ( 'NONE',  ( -0.03824742239841866925, 139.0958210944198470, 488.5995842060523273 ) ) ;
#2556=SURFACE_STYLE_FILL_AREA ( #5872 ) ;
#2559=CARTESIAN_POINT ( 'NONE',  ( -1.135258727068402823E-15, 152.4824555358011082, 478.3411705753777596 ) ) ;
#2562=CARTESIAN_POINT ( 'NONE',  ( -1.000000000000004885, 146.8256012863087108, 507.0490161104376057 ) ) ;
#2563=DIRECTION ( 'NONE',  ( 0.000000000000000000, 0.000000000000000000, 1.000000000000000000 ) ) ;
#2578=LINE ( 'NONE', #13811, #9570 ) ;
#2584=ADVANCED_FACE ( 'NONE', ( #6302 ), #4859, .T. ) ;
#2586=CARTESIAN_POINT ( 'NONE',  ( 0.000000000000000000, 138.7545334744432637, 496.6642397995874489 ) ) ;
#2587=CARTESIAN_POINT ( 'NONE',  ( -80.45457315056674474, 138.8734935819628049, 489.4082602761224621 ) ) ;
#2591=DIRECTION ( 'NONE',  ( 0.000000000000000000, 0.000000000000000000, -1.000000000000000000 ) ) ;
#2605=CARTESIAN_POINT ( 'NONE',  ( -80.68769470327367799, 139.4951205324793477, 500.2397034702902374 ) ) ;
#2606=DIRECTION ( 'NONE',  ( -1.000000000000000000, 0.000000000000000000, 7.715811803773179210E-14 ) ) ;
#2614=DIRECTION ( 'NONE',  ( 1.000000000000000000, 0.000000000000000000, -1.017652531801993019E-13 ) ) ;
#2621=EDGE_LOOP ( 'NONE', ( #20309, #6145, #6277, #1410 ) ) ;
#2632=PRESENTATION_STYLE_ASSIGNMENT (( #4291 ) ) ;
#2637=DIRECTION ( 'NONE',  ( -7.715811803773179210E-14, 0.000000000000000000, -1.000000000000000000 ) ) ;
#2638=DIRECTION ( 'NONE',  ( 0.000000000000000000, -1.000000000000000000, 0.000000000000000000 ) ) ;
#2642=LINE ( 'NONE', #18309, #12582 ) ;
#2662=DIRECTION ( 'NONE',  ( -1.000000000000000000, 0.000000000000000000, 7.715811803773179210E-14 ) ) ;
#2678=LINE ( 'NONE', #15478, #5405 ) ;
#2680=CARTESIAN_POINT ( 'NONE',  ( 0.000000000000000000, 219.7545334744432921, 512.1946179577817020 ) ) ;
#2684=DIRECTION ( 'NONE',  ( 0.000000000000000000, 1.000000000000000000, 0.000000000000000000 ) ) ;
#2687=DIRECTION ( 'NONE',  ( 1.000000000000000000, 0.000000000000000000, 0.000000000000000000 ) ) ;
#2688=CARTESIAN_POINT ( 'NONE',  ( -80.38411152862499875, 139.8075349053433740, 489.3561120975041376 ) ) ;
#2693=CARTESIAN_POINT ( 'NONE',  ( -1.000000000000001554, 152.4824555358010798, 509.3921618609452935 ) ) ;
#2700=COLOUR_RGB ( '', 0.40784314, 0.44705882, 0.49803922) ;
#2723=VERTEX_POINT ( 'NONE', #6923 ) ;
#2724=ORIENTED_EDGE ( 'NONE', *, *, #196, .T. ) ;
#2740=EDGE_CURVE ( 'NONE', #18268, #1517, #13501, .T. ) ;
#2741=AXIS2_PLACEMENT_3D ( 'NONE', #5042, #3500, #8234 ) ;
#2755=EDGE_LOOP ( 'NONE', ( #5305, #2479, #4849, #16937 ) ) ;
#2762=AXIS2_PLACEMENT_3D ( 'NONE', #9949, #14581, #6782 ) ;
#2765=FILL_AREA_STYLE ('',( #4528 ) ) ;
#2769=CIRCLE ( 'NONE', #18548, 8.000000000000007105 ) ;
#2772=ADVANCED_FACE ( 'NONE', ( #5264 ), #2352, .F. ) ;
#2779=VERTEX_POINT ( 'NONE', #3715 ) ;
#2783=CYLINDRICAL_SURFACE ( 'NONE', #12557, 1.000000000000015987 ) ;
#2794=LINE ( 'NONE', #4346, #14233 ) ;
#2814=PRESENTATION_STYLE_ASSIGNMENT (( #15191 ) ) ;
#2815=VERTEX_POINT ( 'NONE', #896 ) ;
#2824=DIRECTION ( 'NONE',  ( 1.000000000000000000, 0.000000000000000000, -0.000000000000000000 ) ) ;
#2830=ORIENTED_EDGE ( 'NONE', *, *, #20322, .T. ) ;
#2838=EDGE_CURVE ( 'NONE', #15103, #2973, #14831, .T. ) ;
#2851=ADVANCED_FACE ( 'NONE', ( #17924 ), #2464, .T. ) ;
#2855=CARTESIAN_POINT ( 'NONE',  ( -38.50085094405407204, 193.0431417881923153, 505.3921618609452935 ) ) ;
#2858=EDGE_CURVE ( 'NONE', #3611, #10328, #7312, .T. ) ;
#2868=MECHANICAL_DESIGN_GEOMETRIC_PRESENTATION_REPRESENTATION('',(#10452),#14394);
#2887=( NAMED_UNIT ( * ) PLANE_ANGLE_UNIT ( ) SI_UNIT ( $, .RADIAN. ) );
#2890=CARTESIAN_POINT ( 'NONE',  ( -0.1304659433170509975, 139.6628864257297380, 500.6059509887651302 ) ) ;
#2893=CARTESIAN_POINT ( 'NONE',  ( -78.99999999999995737, 142.0976792249508662, 502.3210940490797611 ) ) ;
#2899=ORIENTED_EDGE ( 'NONE', *, *, #7794, .T. ) ;
#2917=EDGE_LOOP ( 'NONE', ( #10835, #9546, #6909, #15411 ) ) ;
#2922=LINE ( 'NONE', #13757, #6794 ) ;
#2926=ORIENTED_EDGE ( 'NONE', *, *, #3753, .F. ) ;
#2937=SURFACE_STYLE_FILL_AREA ( #12217 ) ;
#2938=DIRECTION ( 'NONE',  ( -1.000000000000000000, 0.000000000000000000, 7.715811803773179210E-14 ) ) ;
#2944=CARTESIAN_POINT ( 'NONE',  ( -0.6359441111628246768, 138.8819879824800125, 489.5547513090041889 ) ) ;
#2950=ORIENTED_EDGE ( 'NONE', *, *, #8859, .T. ) ;
#2973=VERTEX_POINT ( 'NONE', #19132 ) ;
#2989=DIRECTION ( 'NONE',  ( 1.000000000000000000, 0.000000000000000000, 0.000000000000000000 ) ) ;
#2990=( NAMED_UNIT ( * ) PLANE_ANGLE_UNIT ( ) SI_UNIT ( $, .RADIAN. ) );
#3001=ORIENTED_EDGE ( 'NONE', *, *, #8591, .F. ) ;
#3004=DIRECTION ( 'NONE',  ( 5.099857904826348903E-14, -0.3949357872488050702, -0.9187087263927378178 ) ) ;
#3006=DIRECTION ( 'NONE',  ( -0.000000000000000000, 1.000000000000000000, -0.000000000000000000 ) ) ;
#3010=CARTESIAN_POINT ( 'NONE',  ( 0.6373225965090424383, 139.7798076373073286, 500.8838725201990769 ) ) ;
#3023=EDGE_CURVE ( 'NONE', #17862, #506, #8229, .T. ) ;
#3024=( GEOMETRIC_REPRESENTATION_CONTEXT ( 3 ) GLOBAL_UNCERTAINTY_ASSIGNED_CONTEXT ( ( #10539 ) ) GLOBAL_UNIT_ASSIGNED_CONTEXT ( ( #2320, #16472, #9772 ) ) REPRESENTATION_CONTEXT ( 'NONE', 'WORKASPACE' ) );
#3039=EDGE_CURVE ( 'NONE', #9147, #20015, #15768, .T. ) ;
#3052=EDGE_CURVE ( 'NONE', #4741, #8486, #8021, .T. ) ;
#3055=CARTESIAN_POINT ( 'NONE',  ( -81.00000000000260059, 138.7723821175108014, 490.5025619657601510 ) ) ;
#3061=VECTOR ( 'NONE', #12880, 1000.000000000000000 ) ;
#3086=EDGE_LOOP ( 'NONE', ( #1799, #11503, #11577, #5397, #8148 ) ) ;
#3094=CARTESIAN_POINT ( 'NONE',  ( -81.00000000000260059, 138.7723821175108014, 490.5025619657601510 ) ) ;
#3097=( NAMED_UNIT ( * ) PLANE_ANGLE_UNIT ( ) SI_UNIT ( $, .RADIAN. ) );
#3107=CARTESIAN_POINT ( 'NONE',  ( -1.000000000000012657, 140.8764026050585869, 502.4686618848270996 ) ) ;
#3108=ORIENTED_EDGE ( 'NONE', *, *, #19912, .F. ) ;
#3109=LINE ( 'NONE', #14126, #19553 ) ;
#3113=VECTOR ( 'NONE', #4765, 1000.000000000000000 ) ;
#3114=CIRCLE ( 'NONE', #2116, 8.999999999999952038 ) ;
#3116=EDGE_LOOP ( 'NONE', ( #11356, #4558, #507, #1924 ) ) ;
#3124=COLOUR_RGB ( '', 0.08235294, 0.09019608, 0.10196078) ;
#3131=CARTESIAN_POINT ( 'NONE',  ( 1.181929469892549101, 147.7545334744432921, 491.0690926367356042 ) ) ;
#3137=DIRECTION ( 'NONE',  ( 1.322948291343117631E-12, 0.000000000000000000, 1.000000000000000000 ) ) ;
#3147=VECTOR ( 'NONE', #13155, 1000.000000000000000 ) ;
#3170=VERTEX_POINT ( 'NONE', #8333 ) ;
#3172=CARTESIAN_POINT ( 'NONE',  ( -79.99999999999995737, 141.6406393683236900, 501.8237260975784011 ) ) ;
#3182=LINE ( 'NONE', #15771, #11311 ) ;
#3194=FILL_AREA_STYLE ('',( #1298 ) ) ;
#3202=FILL_AREA_STYLE_COLOUR ( '', #13519 ) ;
#3204=DIRECTION ( 'NONE',  ( -1.000000000000000000, 0.000000000000000000, 0.000000000000000000 ) ) ;
#3209=DIRECTION ( 'NONE',  ( 7.715811803773179210E-14, 0.000000000000000000, 1.000000000000000000 ) ) ;
#3214=AXIS2_PLACEMENT_3D ( 'NONE', #20279, #9364, #12462 ) ;
#3226=CARTESIAN_POINT ( 'NONE',  ( 0.1799495709128176857, 139.9667223049720235, 501.2039705546205823 ) ) ;
#3229=CARTESIAN_POINT ( 'NONE',  ( -38.50085094405407204, 209.4098724938429541, 505.3921618609452935 ) ) ;
#3239=ORIENTED_EDGE ( 'NONE', *, *, #5107, .T. ) ;
#3255=CARTESIAN_POINT ( 'NONE',  ( 0.9999999999999872324, 138.7545334744432637, 488.5655098179835818 ) ) ;
#3256=FILL_AREA_STYLE_COLOUR ( '', #1317 ) ;
#3266=EDGE_CURVE ( 'NONE', #10884, #2779, #962, .T. ) ;
#3268=DIRECTION ( 'NONE',  ( -0.000000000000000000, 1.000000000000000000, -0.000000000000000000 ) ) ;
#3269=CARTESIAN_POINT ( 'NONE',  ( -80.85496986907217831, 140.4048636631002580, 500.8237260975781737 ) ) ;
#3281=LINE ( 'NONE', #9365, #10308 ) ;
#3284=DIRECTION ( 'NONE',  ( -1.000000000000000000, 0.000000000000000000, 1.450371633464475582E-15 ) ) ;
#3290=ORIENTED_EDGE ( 'NONE', *, *, #4726, .F. ) ;
#3306=FILL_AREA_STYLE_COLOUR ( '', #82 ) ;
#3308=EDGE_CURVE ( 'NONE', #5827, #2527, #19830, .T. ) ;
#3319=FACE_OUTER_BOUND ( 'NONE', #178, .T. ) ;
#3323=CIRCLE ( 'NONE', #17472, 9.000000000000007105 ) ;
#3324=CARTESIAN_POINT ( 'NONE',  ( -1.000000012540656069, 140.6662311104242349, 502.2196126213723915 ) ) ;
#3325=ADVANCED_FACE ( 'NONE', ( #6251, #8105, #17367 ), #6158, .F. ) ;
#3326=CYLINDRICAL_SURFACE ( 'NONE', #9809, 1.000000000000000888 ) ;
#3328=DIRECTION ( 'NONE',  ( -5.540106248403443714E-14, 0.06294785234384196737, -0.9980168174361081501 ) ) ;
#3331=DIRECTION ( 'NONE',  ( 1.000000000000000000, -0.000000000000000000, -0.000000000000000000 ) ) ;
#3337=DIRECTION ( 'NONE',  ( -0.000000000000000000, 1.000000000000000000, 0.000000000000000000 ) ) ;
#3340=ORIENTED_EDGE ( 'NONE', *, *, #11511, .F. ) ;
#3355=EDGE_CURVE ( 'NONE', #8340, #14814, #174, .T. ) ;
#3358=ORIENTED_EDGE ( 'NONE', *, *, #17075, .T. ) ;
#3364=CARTESIAN_POINT ( 'NONE',  ( -81.00000000000260059, 139.7703989349477354, 490.5655098180907885 ) ) ;
#3365=ADVANCED_FACE ( 'NONE', ( #12634 ), #18502, .T. ) ;
#3366=CARTESIAN_POINT ( 'NONE',  ( -79.99999999999995737, 216.7545334744432921, 478.3411705753777596 ) ) ;
#3367=CARTESIAN_POINT ( 'NONE',  ( -0.2803133411605864267, 138.8192838135785507, 489.9877526172908233 ) ) ;
#3368=EDGE_LOOP ( 'NONE', ( #952, #2526, #18692, #3681, #11719 ) ) ;
#3373=CARTESIAN_POINT ( 'NONE',  ( -78.99999999591139499, 140.6663224100674370, 502.2197208097303474 ) ) ;
#3390=DIRECTION ( 'NONE',  ( 0.000000000000000000, -1.000000000000000000, 0.000000000000000000 ) ) ;
#3398=( BOUNDED_SURFACE ( )  B_SPLINE_SURFACE ( 3, 2, ( 
 ( #17897, #18192, #16387 ),
 ( #10269, #8619, #16686 ),
 ( #6805, #2536, #11517 ),
 ( #9971, #2221, #16476 ),
 ( #15022, #778, #18090 ),
 ( #19340, #3798, #2129 ),
 ( #19725, #10168, #7102 ),
 ( #16285, #679, #17797 ),
 ( #3987, #4098, #3689 ),
 ( #8441, #2432, #8738 ),
 ( #2325, #14717, #6899 ),
 ( #587, #875, #5537 ) ),
 .UNSPECIFIED., .F., .F., .T. ) 
 B_SPLINE_SURFACE_WITH_KNOTS ( ( 4, 2, 2, 2, 2, 4 ),
 ( 3, 3 ),
 ( 0.001513949667275679917, 0.002304520018506476739, 0.002699805194121875258, 0.003095090369737273344, 0.003885660720968069949, 0.004676231072198866988 ),
 ( 0.000000000000000000, 1.000000000000000000 ),
 .UNSPECIFIED. ) 
 GEOMETRIC_REPRESENTATION_ITEM ( )  RATIONAL_B_SPLINE_SURFACE ( (
 ( 1.000000000000000000, 0.7071067811865475727, 1.000000000000000000),
 ( 1.000000000000000000, 0.7210992828362334794, 1.000000000000000000),
 ( 1.000000000000000000, 0.7304325578646034822, 1.000000000000000000),
 ( 1.000000000000000000, 0.7381509264279376703, 1.000000000000000000),
 ( 1.000000000000000000, 0.7396729138149117366, 1.000000000000000000),
 ( 1.000000000000000000, 0.7411282974412637392, 1.000000000000000000),
 ( 1.000000000000000000, 0.7410425863960605763, 1.000000000000000000),
 ( 1.000000000000000000, 0.7392589090250264450, 1.000000000000000000),
 ( 1.000000000000000000, 0.7360636976591894420, 1.000000000000000000),
 ( 1.000000000000000000, 0.7309106356142509586, 1.000000000000000000),
 ( 1.000000000000000000, 0.7289402462822450746, 1.000000000000000000),
 ( 1.000000000000000000, 0.7290225827585891105, 1.000000000000000000) ) ) 
 REPRESENTATION_ITEM ( '' )  SURFACE ( )  );
#3401=CLOSED_SHELL ( 'NONE', ( #19100, #18033, #138, #2470, #8067, #14919, #10517, #4991, #4858, #11404, #4207, #3325, #2584, #8762, #14077, #8973, #9314, #18177, #14932, #11058, #11196, #12679, #15273, #10854, #9492, #9665, #20058, #7880, #1638, #47, #1316, #2772, #19974, #3825, #4224, #17857, #7509, #17172, #7025, #14765, #15164, #4717, #18684, #16776, #4577, #17293, #10804, #4250, #12276, #17873, #3365, #6522, #2476, #6348, #12630, #12232, #4848, #8479, #4406, #10661, #12525, #19827, #20209, #12640, #11242, #15428, #17807, #17729, #12972, #2274, #4053, #14542 ) ) ;
#3416=( GEOMETRIC_REPRESENTATION_CONTEXT ( 3 ) GLOBAL_UNCERTAINTY_ASSIGNED_CONTEXT ( ( #2509 ) ) GLOBAL_UNIT_ASSIGNED_CONTEXT ( ( #4318, #12244, #1283 ) ) REPRESENTATION_CONTEXT ( 'NONE', 'WORKASPACE' ) );
#3420=LINE ( 'NONE', #6730, #19548 ) ;
#3422=ORIENTED_EDGE ( 'NONE', *, *, #8631, .F. ) ;
#3432=VECTOR ( 'NONE', #11482, 1000.000000000000000 ) ;
#3433=CYLINDRICAL_SURFACE ( 'NONE', #16012, 3.000000000000009770 ) ;
#3437=CARTESIAN_POINT ( 'NONE',  ( 0.08008856490587368260, 141.0493802267578474, 501.4268783641182381 ) ) ;
#3453=ORIENTED_EDGE ( 'NONE', *, *, #1295, .F. ) ;
#3458=CIRCLE ( 'NONE', #14980, 1.000000000000000888 ) ;
#3461=CARTESIAN_POINT ( 'NONE',  ( -44.50085094405407915, 159.0821755739672483, 505.3921618609452935 ) ) ;
#3469=CIRCLE ( 'NONE', #5123, 0.9999999999999974465 ) ;
#3477=CARTESIAN_POINT ( 'NONE',  ( -44.50085094405407915, 175.4489062796178871, 505.3921618609452935 ) ) ;
#3479=ADVANCED_FACE ( 'NONE', ( #7153 ), #5581, .T. ) ;
#3492=ADVANCED_FACE ( 'NONE', ( #18250 ), #4249, .F. ) ;
#3494=LINE ( 'NONE', #11305, #6269 ) ;
#3500=DIRECTION ( 'NONE',  ( 0.000000000000000000, 0.000000000000000000, 1.000000000000000000 ) ) ;
#3508=( GEOMETRIC_REPRESENTATION_CONTEXT ( 3 ) GLOBAL_UNCERTAINTY_ASSIGNED_CONTEXT ( ( #14660 ) ) GLOBAL_UNIT_ASSIGNED_CONTEXT ( ( #19557, #16609, #3913 ) ) REPRESENTATION_CONTEXT ( 'NONE', 'WORKASPACE' ) );
#3514=AXIS2_PLACEMENT_3D ( 'NONE', #7305, #2148, #14731 ) ;
#3515=PRESENTATION_STYLE_ASSIGNMENT (( #204 ) ) ;
#3516=LINE ( 'NONE', #18843, #19199 ) ;
#3526=DIRECTION ( 'NONE',  ( 0.000000000000000000, 0.7642367632649269549, -0.6449357872488920007 ) ) ;
#3528=CIRCLE ( 'NONE', #14050, 1.000000000000015987 ) ;
#3536=CARTESIAN_POINT ( 'NONE',  ( -79.99999999999995737, 152.4824555358011082, 478.3411705753777596 ) ) ;
#3541=DIRECTION ( 'NONE',  ( -1.000000000000000000, 0.000000000000000000, 1.017652531801993019E-13 ) ) ;
#3544=ORIENTED_EDGE ( 'NONE', *, *, #11891, .F. ) ;
#3546=CARTESIAN_POINT ( 'NONE',  ( 0.000000000000000000, 138.7545334744432637, 491.0690926367356042 ) ) ;
#3551=CARTESIAN_POINT ( 'NONE',  ( -82.18192946989277914, 138.7545334744432637, 500.8237260975782874 ) ) ;
#3554=ORIENTED_EDGE ( 'NONE', *, *, #17144, .T. ) ;
#3558=ORIENTED_EDGE ( 'NONE', *, *, #18842, .F. ) ;
#3561=CARTESIAN_POINT ( 'NONE',  ( 0.4745977552357285023, 139.7919181881820236, 489.4271902104604237 ) ) ;
#3567=DIRECTION ( 'NONE',  ( 0.000000000000000000, 0.000000000000000000, -1.000000000000000000 ) ) ;
#3573=LINE ( 'NONE', #661, #7682 ) ;
#3575=LINE ( 'NONE', #8317, #6977 ) ;
#3583=CARTESIAN_POINT ( 'NONE',  ( -80.81398221677214622, 139.7462607834860648, 500.8237260972081799 ) ) ;
#3585=ADVANCED_FACE ( 'NONE', ( #12481 ), #9393, .F. ) ;
#3586=DIRECTION ( 'NONE',  ( 0.000000000000000000, 1.000000000000000000, 0.000000000000000000 ) ) ;
#3596=DIRECTION ( 'NONE',  ( 1.450371633464475582E-15, 0.000000000000000000, 1.000000000000000000 ) ) ;
#3599=EDGE_CURVE ( 'NONE', #1878, #792, #9302, .T. ) ;
#3608=ORIENTED_EDGE ( 'NONE', *, *, #19563, .F. ) ;
#3611=VERTEX_POINT ( 'NONE', #15272 ) ;
#3625=EDGE_CURVE ( 'NONE', #9522, #3885, #13820, .T. ) ;
#3636=CARTESIAN_POINT ( 'NONE',  ( -1.387778780781445676E-14, 138.7545334744432637, 489.5655098179848892 ) ) ;
#3637=DIRECTION ( 'NONE',  ( 0.000000000000000000, 0.7071067811865336949, -0.7071067811865614505 ) ) ;
#3639=DIRECTION ( 'NONE',  ( 1.000000000000000000, 0.000000000000000000, 0.000000000000000000 ) ) ;
#3646=DIRECTION ( 'NONE',  ( -0.000000000000000000, -0.000000000000000000, -1.000000000000000000 ) ) ;
#3651=AXIS2_PLACEMENT_3D ( 'NONE', #14115, #1, #14427 ) ;
#3654=VECTOR ( 'NONE', #12249, 1000.000000000000000 ) ;
#3658=ORIENTED_EDGE ( 'NONE', *, *, #19355, .F. ) ;
#3681=ORIENTED_EDGE ( 'NONE', *, *, #317, .T. ) ;
#3682=CARTESIAN_POINT ( 'NONE',  ( 1.181929469893326257, 138.7545334744432637, 500.8237260975781737 ) ) ;
#3683=SURFACE_STYLE_FILL_AREA ( #2123 ) ;
#3689=CARTESIAN_POINT ( 'NONE',  ( -0.01728972014804384949, 138.7946624528599671, 490.2123583867289653 ) ) ;
#3696=DIRECTION ( 'NONE',  ( 0.000000000000000000, 0.000000000000000000, -1.000000000000000000 ) ) ;
#3698=ORIENTED_EDGE ( 'NONE', *, *, #9646, .F. ) ;
#3710=LINE ( 'NONE', #7120, #112 ) ;
#3715=CARTESIAN_POINT ( 'NONE',  ( -44.50085094405409336, 193.0431417881923153, 505.3921618609452935 ) ) ;
#3722=DIRECTION ( 'NONE',  ( -0.000000000000000000, 0.7071067811865455743, 0.7071067811865493491 ) ) ;
#3725=CARTESIAN_POINT ( 'NONE',  ( -1.135258727068402232E-15, 138.7545334744432637, 478.3411705753777596 ) ) ;
#3726=EDGE_CURVE ( 'NONE', #19976, #2341, #9450, .T. ) ;
#3727=AXIS2_PLACEMENT_3D ( 'NONE', #16925, #8975, #2989 ) ;
#3735=ORIENTED_EDGE ( 'NONE', *, *, #6001, .F. ) ;
#3738=LINE ( 'NONE', #10120, #11197 ) ;
#3744=LINE ( 'NONE', #13043, #16563 ) ;
#3751=AXIS2_PLACEMENT_3D ( 'NONE', #8705, #2513, #19606 ) ;
#3753=EDGE_CURVE ( 'NONE', #11075, #13854, #12433, .T. ) ;
#3755=ORIENTED_EDGE ( 'NONE', *, *, #435, .T. ) ;
#3758=EDGE_LOOP ( 'NONE', ( #7656, #578, #19030, #526, #4213, #15922 ) ) ;
#3769=CARTESIAN_POINT ( 'NONE',  ( 0.000000000000000000, 316.7545334744432353, 515.1946179577817020 ) ) ;
#3771=SPHERICAL_SURFACE ( 'NONE', #10026, 1.000000000000000000 ) ;
#3772=AXIS2_PLACEMENT_3D ( 'NONE', #17318, #10936, #4854 ) ;
#3776=DIRECTION ( 'NONE',  ( 0.000000000000000000, 0.000000000000000000, -1.000000000000000000 ) ) ;
#3786=ORIENTED_EDGE ( 'NONE', *, *, #689, .T. ) ;
#3789=ORIENTED_EDGE ( 'NONE', *, *, #15038, .T. ) ;
#3792=DIRECTION ( 'NONE',  ( 7.714700791774674864E-14, 0.000000000000000000, 1.000000000000000000 ) ) ;
#3795=CARTESIAN_POINT ( 'NONE',  ( -64.99999999999995737, 316.7545334744432353, 475.1454018718993098 ) ) ;
#3798=CARTESIAN_POINT ( 'NONE',  ( 0.1267668549151080015, 138.9617779728525875, 489.0733406692675089 ) ) ;
#3802=( LENGTH_UNIT ( ) NAMED_UNIT ( * ) SI_UNIT ( .MILLI., .METRE. ) );
#3804=AXIS2_PLACEMENT_3D ( 'NONE', #7230, #19575, #13608 ) ;
#3812=ORIENTED_EDGE ( 'NONE', *, *, #5148, .T. ) ;
#3820=CARTESIAN_POINT ( 'NONE',  ( -78.99999999999995737, 138.7545334744432637, 478.3411705753777596 ) ) ;
#3823=CARTESIAN_POINT ( 'NONE',  ( -79.99999999999995737, 216.7545334744432921, 477.3411705753777596 ) ) ;
#3825=ADVANCED_FACE ( 'NONE', ( #5176 ), #11447, .T. ) ;
#3835=CARTESIAN_POINT ( 'NONE',  ( -44.50085094405409336, 193.0431417881923153, 510.3921618609452935 ) ) ;
#3836=VERTEX_POINT ( 'NONE', #2559 ) ;
#3841=CARTESIAN_POINT ( 'NONE',  ( -79.99999999999995737, 216.7545334744432921, 495.1946179577816451 ) ) ;
#3842=ORIENTED_EDGE ( 'NONE', *, *, #9922, .T. ) ;
#3845=CARTESIAN_POINT ( 'NONE',  ( -81.18192946989263703, 138.7545334744432637, 496.6642397995874489 ) ) ;
#3852=EDGE_CURVE ( 'NONE', #2362, #12596, #5659, .T. ) ;
#3865=DIRECTION ( 'NONE',  ( 1.000000000000000000, 0.000000000000000000, -0.000000000000000000 ) ) ;
#3868=UNCERTAINTY_MEASURE_WITH_UNIT (LENGTH_MEASURE( 1.000000000000000082E-05 ), #2343, 'distance_accuracy_value', 'NONE');
#3870=CARTESIAN_POINT ( 'NONE',  ( -38.50085094405407204, 175.4489062796178871, 510.3921618609452935 ) ) ;
#3872=COLOUR_RGB ( '', 0.72549020, 0.75294118, 0.79215686) ;
#3874=CYLINDRICAL_SURFACE ( 'NONE', #5229, 1.000000000000000888 ) ;
#3885=VERTEX_POINT ( 'NONE', #2355 ) ;
#3888=CARTESIAN_POINT ( 'NONE',  ( -1.000000000000012657, 140.1563709946295262, 488.5655098179835818 ) ) ;
#3889=ORIENTED_EDGE ( 'NONE', *, *, #13535, .T. ) ;
#3891=PRESENTATION_STYLE_ASSIGNMENT (( #17996 ) ) ;
#3896=FACE_OUTER_BOUND ( 'NONE', #2374, .T. ) ;
#3904=VERTEX_POINT ( 'NONE', #5470 ) ;
#3908=VERTEX_POINT ( 'NONE', #2243 ) ;
#3913=( NAMED_UNIT ( * ) SI_UNIT ( $, .STERADIAN. ) SOLID_ANGLE_UNIT ( ) );
#3933=EDGE_LOOP ( 'NONE', ( #11920, #16508, #1142, #18920, #7489, #16854, #3340, #2421, #13698, #6768, #5791, #1045, #7979, #2218, #8813, #13971, #4715, #18740, #3422, #19594, #4823, #1820, #1754, #7058 ) ) ;
#3935=PLANE ( 'NONE',  #523 ) ;
#3940=CARTESIAN_POINT ( 'NONE',  ( 2.181929469893224560, 138.7545334744432637, 499.8237260975781169 ) ) ;
#3945=DIRECTION ( 'NONE',  ( 0.000000000000000000, -0.000000000000000000, 1.000000000000000000 ) ) ;
#3959=CARTESIAN_POINT ( 'NONE',  ( -80.99999999999995737, 139.4861549369088323, 500.2186618848270996 ) ) ;
#3962=CARTESIAN_POINT ( 'NONE',  ( -58.16843972078500258, 317.7545334744432353, 485.1700099148404206 ) ) ;
#3964=DIRECTION ( 'NONE',  ( 0.000000000000000000, 0.000000000000000000, 1.000000000000000000 ) ) ;
#3966=CARTESIAN_POINT ( 'NONE',  ( -79.99999999999995737, 316.7545334744432921, 155.1946179577816167 ) ) ;
#3971=DIRECTION ( 'NONE',  ( 0.000000000000000000, 0.000000000000000000, 1.000000000000000000 ) ) ;
#3974=EDGE_LOOP ( 'NONE', ( #17450, #12473, #9773, #12802 ) ) ;
#3975=ADVANCED_FACE ( 'NONE', ( #989 ), #7314, .T. ) ;
#3976=ORIENTED_EDGE ( 'NONE', *, *, #7986, .F. ) ;
#3987=CARTESIAN_POINT ( 'NONE',  ( 0.4913551399758951943, 139.7902036804299826, 489.4365304495848363 ) ) ;
#3991=CARTESIAN_POINT ( 'NONE',  ( 0.000000000000000000, 316.7545334744432353, 0.000000000000000000 ) ) ;
#4000=ORIENTED_EDGE ( 'NONE', *, *, #15809, .T. ) ;
#4006=DIRECTION ( 'NONE',  ( 0.000000000000000000, 0.000000000000000000, -1.000000000000000000 ) ) ;
#4009=SURFACE_STYLE_FILL_AREA ( #6826 ) ;
#4010=DIRECTION ( 'NONE',  ( 3.328238341717372086E-14, 0.000000000000000000, -1.000000000000000000 ) ) ;
#4013=DIRECTION ( 'NONE',  ( 1.000000000000000000, 0.000000000000000000, 0.000000000000000000 ) ) ;
#4021=CIRCLE ( 'NONE', #5340, 8.999999999999952038 ) ;
#4032=( GEOMETRIC_REPRESENTATION_CONTEXT ( 3 ) GLOBAL_UNCERTAINTY_ASSIGNED_CONTEXT ( ( #833 ) ) GLOBAL_UNIT_ASSIGNED_CONTEXT ( ( #11594, #10060, #14698 ) ) REPRESENTATION_CONTEXT ( 'NONE', 'WORKASPACE' ) );
#4041=SURFACE_STYLE_FILL_AREA ( #4160 ) ;
#4053=ADVANCED_FACE ( 'NONE', ( #1394 ), #14008, .F. ) ;
#4055=VECTOR ( 'NONE', #16109, 1000.000000000000000 ) ;
#4056=EDGE_LOOP ( 'NONE', ( #6896, #4654 ) ) ;
#4088=VECTOR ( 'NONE', #9581, 1000.000000000000000 ) ;
#4097=CARTESIAN_POINT ( 'NONE',  ( 0.000000000000000000, 141.3905724437643414, 503.0282008302663144 ) ) ;
#4098=CARTESIAN_POINT ( 'NONE',  ( 0.4533632002511213122, 138.8714365591661704, 489.4163574291068812 ) ) ;
#4100=CARTESIAN_POINT ( 'NONE',  ( 1.181929469892549101, 138.7545334744432637, 491.0690926367356042 ) ) ;
#4102=VECTOR ( 'NONE', #522, 1000.000000000000000 ) ;
#4105=DIRECTION ( 'NONE',  ( -0.000000000000000000, 1.000000000000000000, 0.000000000000000000 ) ) ;
#4110=CARTESIAN_POINT ( 'NONE',  ( 0.000000000000000000, 219.7545334744432921, 515.1946179577817020 ) ) ;
#4113=MECHANICAL_DESIGN_GEOMETRIC_PRESENTATION_REPRESENTATION('',(#1439),#12675);
#4123=CARTESIAN_POINT ( 'NONE',  ( 0.000000000000000000, 316.7545334744432353, 515.1946179577817020 ) ) ;
#4130=DIRECTION ( 'NONE',  ( 0.000000000000000000, 0.000000000000000000, -1.000000000000000000 ) ) ;
#4132=DIRECTION ( 'NONE',  ( 1.000000000000000000, 0.000000000000000000, 3.328238341717372086E-14 ) ) ;
#4140=CARTESIAN_POINT ( 'NONE',  ( -79.99999999999995737, 216.7545334744432921, 501.8237260975782874 ) ) ;
#4144=CIRCLE ( 'NONE', #8423, 9.000000000000007105 ) ;
#4151=ORIENTED_EDGE ( 'NONE', *, *, #11019, .T. ) ;
#4155=UNCERTAINTY_MEASURE_WITH_UNIT (LENGTH_MEASURE( 1.000000000000000082E-05 ), #15597, 'distance_accuracy_value', 'NONE');
#4160=FILL_AREA_STYLE ('',( #18136 ) ) ;
#4163=CARTESIAN_POINT ( 'NONE',  ( -80.46961127677876391, 138.7756291458123883, 490.4424144462261097 ) ) ;
#4171=EDGE_CURVE ( 'NONE', #15133, #19368, #7918, .T. ) ;
#4185=SPHERICAL_SURFACE ( 'NONE', #9504, 1.000000000000000000 ) ;
#4186=CARTESIAN_POINT ( 'NONE',  ( 0.000000000000000000, 139.4861549369088323, 500.2186618848270996 ) ) ;
#4205=FACE_OUTER_BOUND ( 'NONE', #91, .T. ) ;
#4207=ADVANCED_FACE ( 'NONE', ( #1912 ), #8233, .F. ) ;
#4208=SURFACE_STYLE_USAGE ( .BOTH. , #8742 ) ;
#4213=ORIENTED_EDGE ( 'NONE', *, *, #2461, .T. ) ;
#4216=ORIENTED_EDGE ( 'NONE', *, *, #18347, .F. ) ;
#4218=EDGE_CURVE ( 'NONE', #17862, #10840, #15080, .T. ) ;
#4221=ORIENTED_EDGE ( 'NONE', *, *, #1287, .F. ) ;
#4222=CARTESIAN_POINT ( 'NONE',  ( -78.99999999999995737, 146.1184945051221575, 507.7561228916242158 ) ) ;
#4223=LINE ( 'NONE', #2237, #17442 ) ;
#4224=ADVANCED_FACE ( 'NONE', ( #19433 ), #16688, .T. ) ;
#4249=PLANE ( 'NONE',  #7661 ) ;
#4250=ADVANCED_FACE ( 'NONE', ( #3896 ), #7104, .T. ) ;
#4253=VECTOR ( 'NONE', #2270, 1000.000000000000000 ) ;
#4262=VERTEX_POINT ( 'NONE', #14719 ) ;
#4266=VERTEX_POINT ( 'NONE', #4100 ) ;
#4271=( LENGTH_UNIT ( ) NAMED_UNIT ( * ) SI_UNIT ( .MILLI., .METRE. ) );
#4286=DIRECTION ( 'NONE',  ( -0.000000000000000000, 1.000000000000000000, -0.000000000000000000 ) ) ;
#4291=SURFACE_STYLE_USAGE ( .BOTH. , #7192 ) ;
#4297=LINE ( 'NONE', #10578, #403 ) ;
#4301=LINE ( 'NONE', #7405, #19461 ) ;
#4302=ORIENTED_EDGE ( 'NONE', *, *, #1132, .F. ) ;
#4305=ORIENTED_EDGE ( 'NONE', *, *, #19432, .T. ) ;
#4318=( LENGTH_UNIT ( ) NAMED_UNIT ( * ) SI_UNIT ( .MILLI., .METRE. ) );
#4324=CARTESIAN_POINT ( 'NONE',  ( -41.50085094405407915, 159.0821755739672483, 510.3921618609452935 ) ) ;
#4332=ORIENTED_EDGE ( 'NONE', *, *, #19452, .T. ) ;
#4346=CARTESIAN_POINT ( 'NONE',  ( -79.99999999999995737, 140.4048636633015406, 500.8237260975782874 ) ) ;
#4355=AXIS2_PLACEMENT_3D ( 'NONE', #11164, #18688, #1467 ) ;
#4362=CARTESIAN_POINT ( 'NONE',  ( -80.11724004894423956, 140.9328816482941420, 501.3369121427558639 ) ) ;
#4366=DIRECTION ( 'NONE',  ( 7.715811803773179210E-14, 0.000000000000000000, 1.000000000000000000 ) ) ;
#4373=AXIS2_PLACEMENT_3D ( 'NONE', #14880, #2606, #19607 ) ;
#4389=CARTESIAN_POINT ( 'NONE',  ( -44.50085094405410757, 209.4098724938429541, 510.3921618609452935 ) ) ;
#4406=ADVANCED_FACE ( 'NONE', ( #5940 ), #12123, .T. ) ;
#4409=CARTESIAN_POINT ( 'NONE',  ( -80.31054232717158925, 138.7814785482270565, 490.3703103398013354 ) ) ;
#4421=DIRECTION ( 'NONE',  ( 0.000000000000000000, 0.000000000000000000, 1.000000000000000000 ) ) ;
#4422=CARTESIAN_POINT ( 'NONE',  ( -78.99999999999995737, 141.3905724437643698, 484.7051316060566819 ) ) ;
#4426=DIRECTION ( 'NONE',  ( 1.000000000000000000, 0.000000000000000000, 0.000000000000000000 ) ) ;
#4429=AXIS2_PLACEMENT_3D ( 'NONE', #3229, #4880, #1963 ) ;
#4430=VECTOR ( 'NONE', #5275, 1000.000000000000000 ) ;
#4432=VECTOR ( 'NONE', #9502, 1000.000000000000000 ) ;
#4434=CIRCLE ( 'NONE', #8061, 8.000000000000007105 ) ;
#4438=DIRECTION ( 'NONE',  ( 1.000000000000000000, 0.000000000000000000, 0.000000000000000000 ) ) ;
#4440=EDGE_CURVE ( 'NONE', #20158, #17622, #17071, .T. ) ;
#4464=ORIENTED_EDGE ( 'NONE', *, *, #9786, .F. ) ;
#4476=PLANE ( 'NONE',  #16406 ) ;
#4490=ORIENTED_EDGE ( 'NONE', *, *, #16048, .F. ) ;
#4496=LINE ( 'NONE', #10775, #19848 ) ;
#4501=CYLINDRICAL_SURFACE ( 'NONE', #18075, 1.000000000000000888 ) ;
#4503=CARTESIAN_POINT ( 'NONE',  ( 0.000000000000000000, 216.7545334744432921, 205.1946179577815883 ) ) ;
#4504=EDGE_CURVE ( 'NONE', #17622, #12429, #12042, .T. ) ;
#4519=CARTESIAN_POINT ( 'NONE',  ( -79.35594118700021227, 138.8781009637241368, 489.5670100215901357 ) ) ;
#4525=DIRECTION ( 'NONE',  ( 0.000000000000000000, -1.632680918566406547E-16, 1.000000000000000000 ) ) ;
#4526=DIRECTION ( 'NONE',  ( 0.000000000000000000, 0.7642367632649269549, -0.6449357872488920007 ) ) ;
#4528=FILL_AREA_STYLE_COLOUR ( '', #3872 ) ;
#4533=CARTESIAN_POINT ( 'NONE',  ( -1.000000000000019984, 147.7545334744432921, 496.6642397995874489 ) ) ;
#4535=ORIENTED_EDGE ( 'NONE', *, *, #20322, .F. ) ;
#4538=ORIENTED_EDGE ( 'NONE', *, *, #7689, .F. ) ;
#4549=SURFACE_SIDE_STYLE ('',( #18850 ) ) ;
#4551=SURFACE_STYLE_USAGE ( .BOTH. , #12391 ) ;
#4553=ORIENTED_EDGE ( 'NONE', *, *, #5107, .F. ) ;
#4555=DIRECTION ( 'NONE',  ( 0.000000000000000000, 0.7071067811865336949, -0.7071067811865614505 ) ) ;
#4557=VECTOR ( 'NONE', #1992, 1000.000000000000000 ) ;
#4558=ORIENTED_EDGE ( 'NONE', *, *, #19452, .F. ) ;
#4567=CARTESIAN_POINT ( 'NONE',  ( -78.99999999999995737, 144.4616402556298453, 504.6850550797586834 ) ) ;
#4569=CARTESIAN_POINT ( 'NONE',  ( 0.1710018411068576494, 140.8447580977620248, 501.2608735269712383 ) ) ;
#4572=VERTEX_POINT ( 'NONE', #4503 ) ;
#4573=DIRECTION ( 'NONE',  ( 0.000000000000000000, -0.3129478523439812032, 0.9497703099767279555 ) ) ;
#4577=ADVANCED_FACE ( 'NONE', ( #20257 ), #12437, .F. ) ;
#4588=CARTESIAN_POINT ( 'NONE',  ( 0.1178092222713691406, 140.9311717929738279, 501.3355664049633447 ) ) ;
#4604=DIRECTION ( 'NONE',  ( 3.295974604355930324E-14, 3.469446951953611033E-15, -1.000000000000000000 ) ) ;
#4607=EDGE_CURVE ( 'NONE', #645, #9471, #15848, .T. ) ;
#4613=ORIENTED_EDGE ( 'NONE', *, *, #6146, .F. ) ;
#4631=STYLED_ITEM ( 'NONE', ( #1524 ), #6305 ) ;
#4639=ORIENTED_EDGE ( 'NONE', *, *, #18117, .T. ) ;
#4654=ORIENTED_EDGE ( 'NONE', *, *, #7986, .T. ) ;
#4665=DIRECTION ( 'NONE',  ( -1.000000000000000000, 0.000000000000000000, 5.551115123125782702E-14 ) ) ;
#4675=CARTESIAN_POINT ( 'NONE',  ( -81.18192946989275072, 140.4048636633015406, 499.8237260975782874 ) ) ;
#4690=CIRCLE ( 'NONE', #17838, 1.000000000000000888 ) ;
#4694=DIRECTION ( 'NONE',  ( 0.000000000000000000, 0.000000000000000000, -1.000000000000000000 ) ) ;
#4698=DIRECTION ( 'NONE',  ( 0.000000000000000000, 0.000000000000000000, -1.000000000000000000 ) ) ;
#4702=CARTESIAN_POINT ( 'NONE',  ( -1.170604780609792455E-14, 142.0976792249509231, 502.3210940490797611 ) ) ;
#4713=FACE_OUTER_BOUND ( 'NONE', #19789, .T. ) ;
#4714=CARTESIAN_POINT ( 'NONE',  ( -79.03568289232478605, 140.4747598996043507, 501.9652730068947335 ) ) ;
#4715=ORIENTED_EDGE ( 'NONE', *, *, #17733, .F. ) ;
#4717=ADVANCED_FACE ( 'NONE', ( #17981 ), #3874, .T. ) ;
#4726=EDGE_CURVE ( 'NONE', #5319, #6868, #14425, .T. ) ;
#4730=DIRECTION ( 'NONE',  ( 0.000000000000000000, 0.000000000000000000, -1.000000000000000000 ) ) ;
#4734=DIRECTION ( 'NONE',  ( 1.016981637791458695E-13, 0.000000000000000000, 1.000000000000000000 ) ) ;
#4737=AXIS2_PLACEMENT_3D ( 'NONE', #14164, #252, #10875 ) ;
#4739=AXIS2_PLACEMENT_3D ( 'NONE', #1610, #12680, #83 ) ;
#4741=VERTEX_POINT ( 'NONE', #14887 ) ;
#4753=( NAMED_UNIT ( * ) SI_UNIT ( $, .STERADIAN. ) SOLID_ANGLE_UNIT ( ) );
#4754=DIRECTION ( 'NONE',  ( 0.000000000000000000, 0.000000000000000000, -1.000000000000000000 ) ) ;
#4756=DIRECTION ( 'NONE',  ( 0.000000000000000000, -1.000000000000000000, 0.000000000000000000 ) ) ;
#4763=FACE_OUTER_BOUND ( 'NONE', #5183, .T. ) ;
#4765=DIRECTION ( 'NONE',  ( 1.000000000000000000, 0.000000000000000000, 0.000000000000000000 ) ) ;
#4771=EDGE_CURVE ( 'NONE', #19489, #15985, #16755, .T. ) ;
#4775=ORIENTED_EDGE ( 'NONE', *, *, #18807, .T. ) ;
#4778=TOROIDAL_SURFACE ( 'NONE', #13982, 8.000000000000000000, 1.000000000000000000 ) ;
#4781=CIRCLE ( 'NONE', #7421, 3.883636366625808911 ) ;
#4783=CARTESIAN_POINT ( 'NONE',  ( 0.6480199899356283710, 140.4585494651481099, 500.8850776723155036 ) ) ;
#4792=PRESENTATION_STYLE_ASSIGNMENT (( #12611 ) ) ;
#4793=EDGE_CURVE ( 'NONE', #14489, #12201, #14697, .T. ) ;
#4796=FILL_AREA_STYLE ('',( #1342 ) ) ;
#4797=ORIENTED_EDGE ( 'NONE', *, *, #15255, .F. ) ;
#4798=ORIENTED_EDGE ( 'NONE', *, *, #13797, .T. ) ;
#4800=ORIENTED_EDGE ( 'NONE', *, *, #1036, .F. ) ;
#4820=CIRCLE ( 'NONE', #11385, 8.000000000000007105 ) ;
#4823=ORIENTED_EDGE ( 'NONE', *, *, #2740, .F. ) ;
#4828=CARTESIAN_POINT ( 'NONE',  ( -79.91604175977239777, 139.6462705220292548, 500.5714951779720536 ) ) ;
#4840=CARTESIAN_POINT ( 'NONE',  ( -78.99999999999995737, 152.4824555358010798, 501.3921618609452366 ) ) ;
#4848=ADVANCED_FACE ( 'NONE', ( #19806 ), #4185, .T. ) ;
#4849=ORIENTED_EDGE ( 'NONE', *, *, #3308, .T. ) ;
#4854=DIRECTION ( 'NONE',  ( 0.000000000000000000, 0.000000000000000000, -1.000000000000000000 ) ) ;
#4858=ADVANCED_FACE ( 'NONE', ( #1335 ), #16666, .F. ) ;
#4859=PLANE ( 'NONE',  #18291 ) ;
#4864=CARTESIAN_POINT ( 'NONE',  ( 0.000000000000000000, 216.7545334744432921, 515.1946179577817020 ) ) ;
#4865=DIRECTION ( 'NONE',  ( 1.000000000000000000, 0.000000000000000000, 0.000000000000000000 ) ) ;
#4866=DIRECTION ( 'NONE',  ( 0.000000000000000000, 1.000000000000000000, 0.000000000000000000 ) ) ;
#4869=AXIS2_PLACEMENT_3D ( 'NONE', #10082, #16287, #8443 ) ;
#4878=CARTESIAN_POINT ( 'NONE',  ( 0.1064033129882337864, 140.9773519603829754, 501.3703764260786215 ) ) ;
#4880=DIRECTION ( 'NONE',  ( 1.000000000000000000, 0.000000000000000000, 0.000000000000000000 ) ) ;
#4881=VECTOR ( 'NONE', #4698, 1000.000000000000000 ) ;
#4883=PLANE ( 'NONE',  #12805 ) ;
#4888=VERTEX_POINT ( 'NONE', #15514 ) ;
#4893=AXIS2_PLACEMENT_3D ( 'NONE', #6023, #19915, #4366 ) ;
#4896=B_SPLINE_CURVE_WITH_KNOTS ( 'NONE', 3,
 ( #10097, #2235, #14937, #14823, #20269, #5769, #4519, #15350, #13697, #5864, #6178, #4409, #18720, #12061, #18630, #3055 ),
 .UNSPECIFIED., .F., .F.,
 ( 4, 2, 2, 2, 2, 2, 2, 4 ),
 ( 0.000000000000000000, 0.0004237645333845638696, 0.0008475290667691277391, 0.001695058133538260032, 0.002118822666922774624, 0.002542587200307289651, 0.002966351733691804677, 0.003390116267076319703 ),
 .UNSPECIFIED. ) ;
#4909=SHAPE_REPRESENTATION_RELATIONSHIP ( 'NONE' , 'NONE' ,  #16721, #15281 ) ;
#4913=CARTESIAN_POINT ( 'NONE',  ( 0.7149011648340997116, 138.7723821175181911, 490.5025619656413483 ) ) ;
#4920=CARTESIAN_POINT ( 'NONE',  ( -80.42483422545421945, 139.5159773110449350, 500.2902022611505117 ) ) ;
#4947=EDGE_LOOP ( 'NONE', ( #13959, #18297, #7413, #16832 ) ) ;
#4949=DIRECTION ( 'NONE',  ( 0.000000000000000000, -1.000000000000000000, 0.000000000000000000 ) ) ;
#4959=CARTESIAN_POINT ( 'NONE',  ( 0.000000000000000000, 152.4824555358010798, 510.3921618609452935 ) ) ;
#4965=VECTOR ( 'NONE', #755, 1000.000000000000000 ) ;
#4983=CARTESIAN_POINT ( 'NONE',  ( 0.3482790861934039195, 140.6280840731730848, 501.0621025226475922 ) ) ;
#4986=CARTESIAN_POINT ( 'NONE',  ( -79.99999999999995737, 216.7545334744432921, 509.3921618609452935 ) ) ;
#4987=EDGE_LOOP ( 'NONE', ( #8371, #4613, #7623, #3239 ) ) ;
#4991=ADVANCED_FACE ( 'NONE', ( #10963 ), #4883, .F. ) ;
#5003=VERTEX_POINT ( 'NONE', #7867 ) ;
#5012=EDGE_CURVE ( 'NONE', #14814, #14706, #19367, .T. ) ;
#5018=LINE ( 'NONE', #9444, #10647 ) ;
#5030=AXIS2_PLACEMENT_3D ( 'NONE', #12674, #10291, #4734 ) ;
#5035=COLOUR_RGB ( '', 0.09019608, 0.27058824, 0.51372549) ;
#5042=CARTESIAN_POINT ( 'NONE',  ( 0.000000000000000000, 0.000000000000000000, 0.000000000000000000 ) ) ;
#5043=PRESENTATION_STYLE_ASSIGNMENT (( #17237 ) ) ;
#5053=CARTESIAN_POINT ( 'NONE',  ( -1.000000000000000888, 152.4824555358011082, 477.3411705753777596 ) ) ;
#5056=ORIENTED_EDGE ( 'NONE', *, *, #16807, .T. ) ;
#5058=DIRECTION ( 'NONE',  ( 0.000000000000000000, 1.000000000000000000, -0.000000000000000000 ) ) ;
#5059=FACE_OUTER_BOUND ( 'NONE', #11533, .T. ) ;
#5062=CIRCLE ( 'NONE', #10315, 8.000000000000007105 ) ;
#5074=VERTEX_POINT ( 'NONE', #11682 ) ;
#5075=CIRCLE ( 'NONE', #14290, 1.000000000000015987 ) ;
#5078=EDGE_LOOP ( 'NONE', ( #7808, #19375, #12002, #12790, #3755, #5711 ) ) ;
#5083=VERTEX_POINT ( 'NONE', #19591 ) ;
#5085=CARTESIAN_POINT ( 'NONE',  ( -78.99999999999995737, 216.7545334744432921, 510.3921618609452935 ) ) ;
#5091=CARTESIAN_POINT ( 'NONE',  ( -78.99999999949856999, 139.1140930665133908, 488.5333147763630564 ) ) ;
#5098=DIRECTION ( 'NONE',  ( 0.000000000000000000, 0.000000000000000000, -1.000000000000000000 ) ) ;
#5107=EDGE_CURVE ( 'NONE', #14489, #9471, #16346, .T. ) ;
#5112=DIRECTION ( 'NONE',  ( -0.000000000000000000, -1.000000000000000000, 0.000000000000000000 ) ) ;
#5116=CARTESIAN_POINT ( 'NONE',  ( 0.1087494598660525141, 139.9047507171206917, 489.0363018669112876 ) ) ;
#5123=AXIS2_PLACEMENT_3D ( 'NONE', #20277, #10709, #4526 ) ;
#5124=PRESENTATION_STYLE_ASSIGNMENT (( #11488 ) ) ;
#5127=FACE_OUTER_BOUND ( 'NONE', #14151, .T. ) ;
#5128=ORIENTED_EDGE ( 'NONE', *, *, #11262, .T. ) ;
#5134=AXIS2_PLACEMENT_3D ( 'NONE', #5642, #11835, #16585 ) ;
#5148=EDGE_CURVE ( 'NONE', #10328, #10073, #18394, .T. ) ;
#5168=LINE ( 'NONE', #19039, #15359 ) ;
#5176=FACE_OUTER_BOUND ( 'NONE', #8034, .T. ) ;
#5183=EDGE_LOOP ( 'NONE', ( #3976, #9048, #17013, #5325 ) ) ;
#5203=FACE_OUTER_BOUND ( 'NONE', #19235, .T. ) ;
#5209=CARTESIAN_POINT ( 'NONE',  ( -38.50085094405407204, 209.4098724938429541, 510.3921618609452935 ) ) ;
#5213=CARTESIAN_POINT ( 'NONE',  ( 0.7241137275630746828, 139.7735476527001879, 489.5362968091732796 ) ) ;
#5218=EDGE_CURVE ( 'NONE', #5765, #3170, #497, .T. ) ;
#5229=AXIS2_PLACEMENT_3D ( 'NONE', #16451, #6784, #19701 ) ;
#5230=ORIENTED_EDGE ( 'NONE', *, *, #17733, .T. ) ;
#5239=DIRECTION ( 'NONE',  ( 0.000000000000000000, 0.000000000000000000, 1.000000000000000000 ) ) ;
#5244=CARTESIAN_POINT ( 'NONE',  ( 0.000000000000000000, 216.7545334744432921, 495.1946179577816451 ) ) ;
#5249=ORIENTED_EDGE ( 'NONE', *, *, #324, .F. ) ;
#5259=ORIENTED_EDGE ( 'NONE', *, *, #8810, .T. ) ;
#5264=FACE_OUTER_BOUND ( 'NONE', #5699, .T. ) ;
#5265=DIRECTION ( 'NONE',  ( 0.000000000000000000, 0.7071067811865336949, 0.7071067811865614505 ) ) ;
#5273=EDGE_CURVE ( 'NONE', #6469, #10221, #9877, .T. ) ;
#5275=DIRECTION ( 'NONE',  ( -0.000000000000000000, -1.000000000000000000, 0.000000000000000000 ) ) ;
#5278=CARTESIAN_POINT ( 'NONE',  ( 0.000000000000000000, 139.4861549369088323, 500.2186618848270996 ) ) ;
#5281=VECTOR ( 'NONE', #16575, 1000.000000000000000 ) ;
#5286=DIRECTION ( 'NONE',  ( -1.000000000000000000, 0.000000000000000000, -1.135258727068399668E-15 ) ) ;
#5296=CARTESIAN_POINT ( 'NONE',  ( 1.181929469892510243, 216.7545334744432921, 490.5655098179833544 ) ) ;
#5297=DIRECTION ( 'NONE',  ( -1.000000000000000000, 0.000000000000000000, -0.000000000000000000 ) ) ;
#5304=VECTOR ( 'NONE', #8360, 1000.000000000000114 ) ;
#5305=ORIENTED_EDGE ( 'NONE', *, *, #15207, .T. ) ;
#5315=DIRECTION ( 'NONE',  ( -0.000000000000000000, -1.000000000000000000, -0.000000000000000000 ) ) ;
#5319=VERTEX_POINT ( 'NONE', #8236 ) ;
#5324=DIRECTION ( 'NONE',  ( 1.000000000000000000, 0.000000000000000000, -1.322948291343117631E-12 ) ) ;
#5325=ORIENTED_EDGE ( 'NONE', *, *, #7873, .F. ) ;
#5326=CIRCLE ( 'NONE', #18455, 1.000000000000000888 ) ;
#5328=ORIENTED_EDGE ( 'NONE', *, *, #15391, .T. ) ;
#5339=CYLINDRICAL_SURFACE ( 'NONE', #13627, 1.000000000000000888 ) ;
#5340=AXIS2_PLACEMENT_3D ( 'NONE', #8437, #16179, #3792 ) ;
#5354=EDGE_LOOP ( 'NONE', ( #16645, #1779, #10978, #10701 ) ) ;
#5358=DIRECTION ( 'NONE',  ( 0.000000000000000000, -1.000000000000000000, 0.000000000000000000 ) ) ;
#5362=EDGE_CURVE ( 'NONE', #1465, #5074, #1594, .T. ) ;
#5363=VECTOR ( 'NONE', #10626, 1000.000000000000000 ) ;
#5365=SURFACE_SIDE_STYLE ('',( #4009 ) ) ;
#5373=STYLED_ITEM ( 'NONE', ( #2632 ), #8230 ) ;
#5397=ORIENTED_EDGE ( 'NONE', *, *, #12250, .T. ) ;
#5400=VECTOR ( 'NONE', #11617, 1000.000000000000000 ) ;
#5404=AXIS2_PLACEMENT_3D ( 'NONE', #7515, #15139, #15244 ) ;
#5405=VECTOR ( 'NONE', #14027, 1000.000000000000000 ) ;
#5418=LINE ( 'NONE', #17978, #7547 ) ;
#5428=CARTESIAN_POINT ( 'NONE',  ( -41.50085094405408626, 209.4098724938429541, 505.3921618609452935 ) ) ;
#5430=EDGE_LOOP ( 'NONE', ( #1615, #6034, #9826, #11300 ) ) ;
#5433=EDGE_LOOP ( 'NONE', ( #16722, #7800, #17698, #15473 ) ) ;
#5434=MECHANICAL_DESIGN_GEOMETRIC_PRESENTATION_REPRESENTATION('',(#19558),#13993);
#5438=CARTESIAN_POINT ( 'NONE',  ( -82.18192946989277914, 216.7545334744432921, 500.8237260975782874 ) ) ;
#5442=CARTESIAN_POINT ( 'NONE',  ( -80.99999999999995737, 216.7545334744432921, 501.8237260975782874 ) ) ;
#5452=ORIENTED_EDGE ( 'NONE', *, *, #16949, .T. ) ;
#5462=SURFACE_SIDE_STYLE ('',( #8758 ) ) ;
#5463=AXIS2_PLACEMENT_3D ( 'NONE', #18133, #10321, #2489 ) ;
#5470=CARTESIAN_POINT ( 'NONE',  ( -64.99999999999995737, 316.7545334744432353, 475.1454018718993098 ) ) ;
#5471=CARTESIAN_POINT ( 'NONE',  ( -79.99999999999995737, 139.2066006846527841, 488.2525619656396429 ) ) ;
#5490=VERTEX_POINT ( 'NONE', #15546 ) ;
#5506=( BOUNDED_SURFACE ( )  B_SPLINE_SURFACE ( 3, 2, ( 
 ( #10326, #19781, #15074 ),
 ( #15277, #1122, #921 ),
 ( #7245, #13527, #4163 ),
 ( #5897, #10435, #9095 ),
 ( #16829, #2587, #7342 ),
 ( #2688, #19588, #19991 ),
 ( #13622, #12088, #10627 ),
 ( #8977, #7457, #8503 ),
 ( #14455, #10195, #13313 ),
 ( #704, #19564, #11257 ),
 ( #19757, #11371, #5091 ),
 ( #19077, #5471, #14838 ) ),
 .UNSPECIFIED., .F., .F., .T. ) 
 B_SPLINE_SURFACE_WITH_KNOTS ( ( 4, 2, 2, 2, 2, 4 ),
 ( 3, 3 ),
 ( 0.001338278704687140058, 0.002129672239503333821, 0.002525369006911430594, 0.002921065774319527367, 0.003712459309135720913, 0.004503852843951914459 ),
 ( 0.000000000000000000, 1.000000000000000000 ),
 .UNSPECIFIED. ) 
 GEOMETRIC_REPRESENTATION_ITEM ( )  RATIONAL_B_SPLINE_SURFACE ( (
 ( 1.000000000000000000, 0.7290225827585891105, 1.000000000000000000),
 ( 1.000000000000000000, 0.7289486400731624016, 1.000000000000000000),
 ( 1.000000000000000000, 0.7309044250879849214, 1.000000000000000000),
 ( 1.000000000000000000, 0.7347910907188455187, 1.000000000000000000),
 ( 1.000000000000000000, 0.7362115201279648691, 1.000000000000000000),
 ( 1.000000000000000000, 0.7387494832161207725, 1.000000000000000000),
 ( 1.000000000000000000, 0.7398605621277711819, 1.000000000000000000),
 ( 1.000000000000000000, 0.7416352795026123212, 1.000000000000000000),
 ( 1.000000000000000000, 0.7406868835584125010, 1.000000000000000000),
 ( 1.000000000000000000, 0.7304426651937115933, 1.000000000000000000),
 ( 1.000000000000000000, 0.7210170799402795261, 1.000000000000000000),
 ( 1.000000000000000000, 0.7071067811865475727, 1.000000000000000000) ) ) 
 REPRESENTATION_ITEM ( '' )  SURFACE ( )  );
#5509=DIRECTION ( 'NONE',  ( -1.000000000000000000, 0.000000000000000000, 5.551115123125782702E-14 ) ) ;
#5511=DIRECTION ( 'NONE',  ( 1.025567617263343161E-15, 0.7071067811865455743, 0.7071067811865493491 ) ) ;
#5529=ORIENTED_EDGE ( 'NONE', *, *, #18808, .T. ) ;
#5537=CARTESIAN_POINT ( 'NONE',  ( 1.000000000002633893, 138.7723821175183900, 490.5025619656395861 ) ) ;
#5541=PLANE ( 'NONE',  #5134 ) ;
#5544=AXIS2_PLACEMENT_3D ( 'NONE', #13077, #11399, #567 ) ;
#5552=EDGE_CURVE ( 'NONE', #2527, #16622, #7358, .T. ) ;
#5560=DIRECTION ( 'NONE',  ( 0.000000000000000000, 0.000000000000000000, 1.000000000000000000 ) ) ;
#5562=CARTESIAN_POINT ( 'NONE',  ( -38.50085094405407204, 175.4489062796178871, 505.3921618609452935 ) ) ;
#5563=CARTESIAN_POINT ( 'NONE',  ( 0.000000000000000000, 219.7545334744432921, 512.1946179577817020 ) ) ;
#5565=ADVANCED_FACE ( 'NONE', ( #18363 ), #8805, .F. ) ;
#5567=AXIS2_PLACEMENT_3D ( 'NONE', #8785, #19772, #18345 ) ;
#5573=ORIENTED_EDGE ( 'NONE', *, *, #8859, .F. ) ;
#5574=DIRECTION ( 'NONE',  ( -1.000000000000000000, -0.000000000000000000, 0.000000000000000000 ) ) ;
#5577=CARTESIAN_POINT ( 'NONE',  ( -82.18192946989240966, 216.7545334744432921, 489.5655098179820470 ) ) ;
#5578=CARTESIAN_POINT ( 'NONE',  ( 1.181929469893224560, 139.4861549369088323, 500.2186618848270996 ) ) ;
#5581=PLANE ( 'NONE',  #10957 ) ;
#5586=EDGE_LOOP ( 'NONE', ( #2101, #7745, #20103, #10012 ) ) ;
#5625=ORIENTED_EDGE ( 'NONE', *, *, #15759, .T. ) ;
#5626=EDGE_LOOP ( 'NONE', ( #3558, #5789, #5056, #614 ) ) ;
#5631=DIRECTION ( 'NONE',  ( 0.000000000000000000, -0.3129478523439812032, 0.9497703099767278445 ) ) ;
#5639=DIRECTION ( 'NONE',  ( -8.027491443112700323E-16, -0.7071067811865504593, 0.7071067811865445751 ) ) ;
#5642=CARTESIAN_POINT ( 'NONE',  ( -44.50085094405407915, 175.4489062796178871, 505.3921618609452935 ) ) ;
#5659=LINE ( 'NONE', #17821, #5844 ) ;
#5679=AXIS2_PLACEMENT_3D ( 'NONE', #13870, #1685, #1260 ) ;
#5687=CARTESIAN_POINT ( 'NONE',  ( -79.99999999999995737, 316.7545334744432353, 515.1946179577817020 ) ) ;
#5692=VECTOR ( 'NONE', #4865, 1000.000000000000000 ) ;
#5696=CIRCLE ( 'NONE', #2051, 0.9999999999999964473 ) ;
#5698=PRODUCT_DEFINITION ( 'UNKNOWN', '', #411, #14817 ) ;
#5699=EDGE_LOOP ( 'NONE', ( #7510, #17833, #15708, #8867 ) ) ;
#5700=EDGE_LOOP ( 'NONE', ( #20290, #3290, #8316, #11743 ) ) ;
#5710=CARTESIAN_POINT ( 'NONE',  ( -80.58226053856785143, 140.4824639777437199, 500.9116485922544371 ) ) ;
#5711=ORIENTED_EDGE ( 'NONE', *, *, #13666, .T. ) ;
#5725=EDGE_CURVE ( 'NONE', #2779, #584, #11512, .T. ) ;
#5741=EDGE_CURVE ( 'NONE', #2973, #7546, #19094, .T. ) ;
#5764=UNCERTAINTY_MEASURE_WITH_UNIT (LENGTH_MEASURE( 1.000000000000000082E-05 ), #17375, 'distance_accuracy_value', 'NONE');
#5765=VERTEX_POINT ( 'NONE', #16153 ) ;
#5769=CARTESIAN_POINT ( 'NONE',  ( -79.22030824640687285, 138.9228415808856596, 489.3162532734729098 ) ) ;
#5770=AXIS2_PLACEMENT_3D ( 'NONE', #12816, #6130, #4665 ) ;
#5771=DIRECTION ( 'NONE',  ( -1.000000000000000000, -0.000000000000000000, -1.135258727068399668E-15 ) ) ;
#5781=SURFACE_STYLE_FILL_AREA ( #2765 ) ;
#5783=DIRECTION ( 'NONE',  ( -0.000000000000000000, -0.000000000000000000, 1.000000000000000000 ) ) ;
#5789=ORIENTED_EDGE ( 'NONE', *, *, #18132, .F. ) ;
#5791=ORIENTED_EDGE ( 'NONE', *, *, #19579, .F. ) ;
#5799=DIRECTION ( 'NONE',  ( -1.000000000000000000, 0.000000000000000000, 1.450371633464475582E-15 ) ) ;
#5802=CARTESIAN_POINT ( 'NONE',  ( 0.000000000000000000, 147.7545334744432921, 491.0690926367356042 ) ) ;
#5806=LINE ( 'NONE', #15774, #15215 ) ;
#5815=EDGE_LOOP ( 'NONE', ( #9706, #11632, #17913, #4151 ) ) ;
#5824=CARTESIAN_POINT ( 'NONE',  ( -21.85283368562565443, 319.7545334744432353, 485.1700099148404774 ) ) ;
#5825=FACE_OUTER_BOUND ( 'NONE', #1519, .T. ) ;
#5827=VERTEX_POINT ( 'NONE', #20000 ) ;
#5829=CARTESIAN_POINT ( 'NONE',  ( -78.99999999999995737, 152.4824555358011082, 486.3411705753778165 ) ) ;
#5830=PRODUCT_CONTEXT ( 'NONE', #2487, 'mechanical' ) ;
#5837=CARTESIAN_POINT ( 'NONE',  ( -79.99999999999995737, 316.7545334744432353, 495.1946179577816451 ) ) ;
#5839=DIRECTION ( 'NONE',  ( -1.132388935707081510E-15, 0.000000000000000000, 1.000000000000000000 ) ) ;
#5844=VECTOR ( 'NONE', #4013, 1000.000000000000000 ) ;
#5848=EDGE_CURVE ( 'NONE', #11820, #4266, #17774, .T. ) ;
#5849=CARTESIAN_POINT ( 'NONE',  ( 0.000000000000000000, 146.1184945051222428, 479.9772095446988374 ) ) ;
#5850=PLANE ( 'NONE',  #12941 ) ;
#5856=( GEOMETRIC_REPRESENTATION_CONTEXT ( 3 ) GLOBAL_UNCERTAINTY_ASSIGNED_CONTEXT ( ( #11031 ) ) GLOBAL_UNIT_ASSIGNED_CONTEXT ( ( #4271, #7474, #13744 ) ) REPRESENTATION_CONTEXT ( 'NONE', 'WORKASPACE' ) );
#5861=ORIENTED_EDGE ( 'NONE', *, *, #8169, .F. ) ;
#5864=CARTESIAN_POINT ( 'NONE',  ( -79.94176149790892794, 138.7993301623293121, 490.1678215211853740 ) ) ;
#5870=DIRECTION ( 'NONE',  ( -0.000000000000000000, -1.000000000000000000, -0.000000000000000000 ) ) ;
#5872=FILL_AREA_STYLE ('',( #10296 ) ) ;
#5882=ORIENTED_EDGE ( 'NONE', *, *, #11008, .F. ) ;
#5897=CARTESIAN_POINT ( 'NONE',  ( -80.55146305734733403, 139.7860373442720743, 489.4617291895204971 ) ) ;
#5917=CARTESIAN_POINT ( 'NONE',  ( 2.181929469893403528, 140.4048636633015406, 500.8237260975780600 ) ) ;
#5919=CIRCLE ( 'NONE', #11181, 1.000000000000000888 ) ;
#5928=DIRECTION ( 'NONE',  ( 1.000000000000000000, 0.000000000000000000, 0.000000000000000000 ) ) ;
#5934=CARTESIAN_POINT ( 'NONE',  ( -81.18192946989243808, 139.7703989349477354, 490.5655098180907885 ) ) ;
#5940=FACE_OUTER_BOUND ( 'NONE', #19537, .T. ) ;
#5944=( NAMED_UNIT ( * ) PLANE_ANGLE_UNIT ( ) SI_UNIT ( $, .RADIAN. ) );
#5947=ORIENTED_EDGE ( 'NONE', *, *, #1132, .T. ) ;
#5954=ORIENTED_EDGE ( 'NONE', *, *, #10655, .F. ) ;
#5961=STYLED_ITEM ( 'NONE', ( #10151 ), #12040 ) ;
#5968=DIRECTION ( 'NONE',  ( -1.000000000000000000, 0.000000000000000000, 0.000000000000000000 ) ) ;
#5978=FACE_OUTER_BOUND ( 'NONE', #20185, .T. ) ;
#5994=FACE_OUTER_BOUND ( 'NONE', #16237, .T. ) ;
#5996=CARTESIAN_POINT ( 'NONE',  ( -0.008242336927396939905, 139.6212446359134276, 500.5185750710210186 ) ) ;
#6001=EDGE_CURVE ( 'NONE', #11075, #15757, #18086, .T. ) ;
#6006=( GEOMETRIC_REPRESENTATION_CONTEXT ( 3 ) GLOBAL_UNCERTAINTY_ASSIGNED_CONTEXT ( ( #8149 ) ) GLOBAL_UNIT_ASSIGNED_CONTEXT ( ( #16682, #1161, #13763 ) ) REPRESENTATION_CONTEXT ( 'NONE', 'WORKASPACE' ) );
#6017=CIRCLE ( 'NONE', #6346, 1.000000000000000888 ) ;
#6023=CARTESIAN_POINT ( 'NONE',  ( 2.181929469893301832, 138.7545334744432637, 500.8237260975780600 ) ) ;
#6034=ORIENTED_EDGE ( 'NONE', *, *, #16724, .T. ) ;
#6040=EDGE_LOOP ( 'NONE', ( #13426, #13266, #17909, #15322 ) ) ;
#6041=CARTESIAN_POINT ( 'NONE',  ( 2.181929469892549545, 139.7545334744432637, 491.0690926367356042 ) ) ;
#6046=DIRECTION ( 'NONE',  ( -1.000000000000000000, -0.000000000000000000, -0.000000000000000000 ) ) ;
#6059=STYLED_ITEM ( 'NONE', ( #4792 ), #19095 ) ;
#6064=( GEOMETRIC_REPRESENTATION_CONTEXT ( 3 ) GLOBAL_UNCERTAINTY_ASSIGNED_CONTEXT ( ( #16540 ) ) GLOBAL_UNIT_ASSIGNED_CONTEXT ( ( #19040, #11224, #4753 ) ) REPRESENTATION_CONTEXT ( 'NONE', 'WORKASPACE' ) );
#6073=ORIENTED_EDGE ( 'NONE', *, *, #890, .T. ) ;
#6076=DIRECTION ( 'NONE',  ( 5.551115123125777022E-14, 0.000000000000000000, -1.000000000000000000 ) ) ;
#6080=PRESENTATION_STYLE_ASSIGNMENT (( #13891 ) ) ;
#6084=TOROIDAL_SURFACE ( 'NONE', #12321, 8.000000000000000000, 1.000000000000000000 ) ;
#6094=EDGE_LOOP ( 'NONE', ( #11722, #19462, #4535, #15885 ) ) ;
#6096=( LENGTH_UNIT ( ) NAMED_UNIT ( * ) SI_UNIT ( .MILLI., .METRE. ) );
#6097=ORIENTED_EDGE ( 'NONE', *, *, #5725, .T. ) ;
#6098=ORIENTED_EDGE ( 'NONE', *, *, #7625, .T. ) ;
#6101=CARTESIAN_POINT ( 'NONE',  ( 1.181929469893326257, 216.7545334744432921, 500.8237260975781737 ) ) ;
#6115=CARTESIAN_POINT ( 'NONE',  ( 2.181929469893301832, 216.7545334744432921, 500.8237260975780600 ) ) ;
#6117=EDGE_CURVE ( 'NONE', #1591, #8486, #11667, .T. ) ;
#6130=DIRECTION ( 'NONE',  ( -5.551115123125782071E-14, 1.697225763491249802E-27, -1.000000000000000000 ) ) ;
#6133=CARTESIAN_POINT ( 'NONE',  ( -0.8398228660021732628, 140.2112360712614532, 501.5757544859369546 ) ) ;
#6144=( NAMED_UNIT ( * ) SI_UNIT ( $, .STERADIAN. ) SOLID_ANGLE_UNIT ( ) );
#6145=ORIENTED_EDGE ( 'NONE', *, *, #9618, .T. ) ;
#6146=EDGE_CURVE ( 'NONE', #12201, #3904, #3738, .T. ) ;
#6149=EDGE_LOOP ( 'NONE', ( #9078, #139 ) ) ;
#6152=VERTEX_POINT ( 'NONE', #3536 ) ;
#6153=CARTESIAN_POINT ( 'NONE',  ( 0.5831304756500845787, 140.4822067609526925, 500.9113485223598445 ) ) ;
#6158=PLANE ( 'NONE',  #18176 ) ;
#6169=EDGE_CURVE ( 'NONE', #625, #5490, #11828, .T. ) ;
#6170=CARTESIAN_POINT ( 'NONE',  ( -1.000000000000012657, 139.2066006846527841, 488.2525619656395861 ) ) ;
#6178=CARTESIAN_POINT ( 'NONE',  ( -80.05917220250364608, 138.7922018492437530, 490.2440936989472675 ) ) ;
#6184=FACE_OUTER_BOUND ( 'NONE', #2917, .T. ) ;
#6191=AXIS2_PLACEMENT_3D ( 'NONE', #11045, #17632, #6720 ) ;
#6198=ORIENTED_EDGE ( 'NONE', *, *, #18547, .T. ) ;
#6217=EDGE_CURVE ( 'NONE', #4888, #1517, #9223, .T. ) ;
#6218=ORIENTED_EDGE ( 'NONE', *, *, #4607, .T. ) ;
#6225=CARTESIAN_POINT ( 'NONE',  ( 0.9068665838271406932, 139.7462607865923871, 500.8237261029128717 ) ) ;
#6251=FACE_BOUND ( 'NONE', #3974, .T. ) ;
#6254=AXIS2_PLACEMENT_3D ( 'NONE', #17721, #512, #605 ) ;
#6269=VECTOR ( 'NONE', #5239, 1000.000000000000000 ) ;
#6273=CARTESIAN_POINT ( 'NONE',  ( -80.29785759403569045, 140.6759013589731353, 501.1085235032808214 ) ) ;
#6275=CARTESIAN_POINT ( 'NONE',  ( -38.50085094405407204, 193.0431417881923153, 510.3921618609452935 ) ) ;
#6277=ORIENTED_EDGE ( 'NONE', *, *, #15595, .F. ) ;
#6280=CARTESIAN_POINT ( 'NONE',  ( -58.16843972078500258, 319.7545334744432353, 481.2863735482146126 ) ) ;
#6281=DIRECTION ( 'NONE',  ( 7.715811803773179210E-14, 0.000000000000000000, 1.000000000000000000 ) ) ;
#6284=EDGE_CURVE ( 'NONE', #10076, #4572, #12478, .T. ) ;
#6302=FACE_OUTER_BOUND ( 'NONE', #19846, .T. ) ;
#6305=ADVANCED_FACE ( 'NONE', ( #18954 ), #20193, .F. ) ;
#6310=CARTESIAN_POINT ( 'NONE',  ( 0.3975717331714440639, 139.5287482107642631, 500.3163965736156911 ) ) ;
#6312=DIRECTION ( 'NONE',  ( -0.000000000000000000, -0.000000000000000000, -1.000000000000000000 ) ) ;
#6319=DIRECTION ( 'NONE',  ( 0.000000000000000000, 1.000000000000000000, 0.000000000000000000 ) ) ;
#6325=FACE_OUTER_BOUND ( 'NONE', #740, .T. ) ;
#6326=DIRECTION ( 'NONE',  ( -0.000000000000000000, 1.000000000000000000, 0.000000000000000000 ) ) ;
#6327=DIRECTION ( 'NONE',  ( 0.000000000000000000, 0.000000000000000000, -1.000000000000000000 ) ) ;
#6332=SURFACE_SIDE_STYLE ('',( #33 ) ) ;
#6339=AXIS2_PLACEMENT_3D ( 'NONE', #14461, #1775, #11475 ) ;
#6341=EDGE_LOOP ( 'NONE', ( #15203, #17145, #18172 ) ) ;
#6346=AXIS2_PLACEMENT_3D ( 'NONE', #12174, #16737, #7455 ) ;
#6348=ADVANCED_FACE ( 'NONE', ( #14524 ), #19453, .T. ) ;
#6357=( LENGTH_UNIT ( ) NAMED_UNIT ( * ) SI_UNIT ( .MILLI., .METRE. ) );
#6363=CARTESIAN_POINT ( 'NONE',  ( 0.000000000000000000, 138.7723821175108014, 490.5025619657601510 ) ) ;
#6374=CARTESIAN_POINT ( 'NONE',  ( -79.59571519198017597, 139.7910723461943974, 500.8594560506689390 ) ) ;
#6377=DIRECTION ( 'NONE',  ( 1.000000000000000000, 0.000000000000000000, 0.000000000000000000 ) ) ;
#6395=AXIS2_PLACEMENT_3D ( 'NONE', #11972, #5574, #15938 ) ;
#6397=VERTEX_POINT ( 'NONE', #11226 ) ;
#6400=( NAMED_UNIT ( * ) PLANE_ANGLE_UNIT ( ) SI_UNIT ( $, .RADIAN. ) );
#6407=AXIS2_PLACEMENT_3D ( 'NONE', #5296, #11886, #12756 ) ;
#6411=AXIS2_PLACEMENT_3D ( 'NONE', #14998, #16947, #8806 ) ;
#6413=CIRCLE ( 'NONE', #10336, 9.000000000000007105 ) ;
#6419=DIRECTION ( 'NONE',  ( -0.000000000000000000, -0.6449357872488783450, -0.7642367632649385012 ) ) ;
#6423=VECTOR ( 'NONE', #15594, 1000.000000000000000 ) ;
#6425=VECTOR ( 'NONE', #20288, 1000.000000000000000 ) ;
#6436=CARTESIAN_POINT ( 'NONE',  ( 0.2985174824345476208, 140.6753058650092498, 501.1079383018479803 ) ) ;
#6441=DIRECTION ( 'NONE',  ( 1.000000000000000000, -0.000000000000000000, -0.000000000000000000 ) ) ;
#6445=PLANE ( 'NONE',  #4355 ) ;
#6454=AXIS2_PLACEMENT_3D ( 'NONE', #1205, #4438, #10616 ) ;
#6460=CARTESIAN_POINT ( 'NONE',  ( 1.181929469892510243, 139.7703989349544145, 490.5655098179848892 ) ) ;
#6469=VERTEX_POINT ( 'NONE', #15044 ) ;
#6474=CARTESIAN_POINT ( 'NONE',  ( -81.00000000000085265, 139.7462607836631321, 500.8237260975782874 ) ) ;
#6479=DIRECTION ( 'NONE',  ( -1.000000000000000000, 0.000000000000000000, -0.000000000000000000 ) ) ;
#6480=AXIS2_PLACEMENT_3D ( 'NONE', #17889, #957, #5839 ) ;
#6496=ORIENTED_EDGE ( 'NONE', *, *, #6117, .F. ) ;
#6500=SURFACE_STYLE_FILL_AREA ( #14331 ) ;
#6506=CARTESIAN_POINT ( 'NONE',  ( 0.9999999999997842837, 139.4861549369088323, 500.2186618848270996 ) ) ;
#6509=( NAMED_UNIT ( * ) SI_UNIT ( $, .STERADIAN. ) SOLID_ANGLE_UNIT ( ) );
#6516=AXIS2_PLACEMENT_3D ( 'NONE', #14247, #7963, #16036 ) ;
#6522=ADVANCED_FACE ( 'NONE', ( #8942 ), #18219, .T. ) ;
#6528=B_SPLINE_CURVE_WITH_KNOTS ( 'NONE', 3,
 ( #3959, #10348, #2605, #9109, #16543, #18273, #1137, #18157, #2398, #15397, #18465, #13542, #7171, #16659 ),
 .UNSPECIFIED., .F., .F.,
 ( 4, 2, 2, 2, 2, 2, 4 ),
 ( 0.000000000000000000, 0.0004665341218959795865, 0.0009330682437919591730, 0.001866136487584075772, 0.002332670609480022670, 0.002799204731375969351, 0.003732272975167592963 ),
 .UNSPECIFIED. ) ;
#6531=CARTESIAN_POINT ( 'NONE',  ( 0.01793673982740404474, 141.2822582158146929, 501.5991098895786990 ) ) ;
#6535=DIRECTION ( 'NONE',  ( -1.000000000000000000, 0.000000000000000000, 0.000000000000000000 ) ) ;
#6556=CARTESIAN_POINT ( 'NONE',  ( -79.99999999999995737, 140.1563709946295262, 488.5655098179835818 ) ) ;
#6559=EDGE_CURVE ( 'NONE', #17453, #19090, #20028, .T. ) ;
#6571=AXIS2_PLACEMENT_3D ( 'NONE', #8107, #17369, #19108 ) ;
#6576=DIRECTION ( 'NONE',  ( -1.135258727068399865E-15, -0.000000000000000000, 1.000000000000000000 ) ) ;
#6577=CARTESIAN_POINT ( 'NONE',  ( -80.01784145024733164, 141.2836236309851188, 501.5999977085803039 ) ) ;
#6585=ORIENTED_EDGE ( 'NONE', *, *, #11501, .T. ) ;
#6589=DIRECTION ( 'NONE',  ( -0.000000000000000000, -1.000000000000000000, -0.000000000000000000 ) ) ;
#6615=DIRECTION ( 'NONE',  ( -0.000000000000000000, 1.000000000000000000, -0.000000000000000000 ) ) ;
#6617=EDGE_CURVE ( 'NONE', #3904, #20015, #15866, .T. ) ;
#6627=ORIENTED_EDGE ( 'NONE', *, *, #6284, .T. ) ;
#6634=DIRECTION ( 'NONE',  ( 0.000000000000000000, -1.000000000000000000, 0.000000000000000000 ) ) ;
#6642=CARTESIAN_POINT ( 'NONE',  ( 1.181929469892510243, 139.7703989349544145, 490.5655098179848892 ) ) ;
#6657=EDGE_CURVE ( 'NONE', #10076, #2362, #3494, .T. ) ;
#6664=ORIENTED_EDGE ( 'NONE', *, *, #876, .F. ) ;
#6666=( NAMED_UNIT ( * ) SI_UNIT ( $, .STERADIAN. ) SOLID_ANGLE_UNIT ( ) );
#6669=CYLINDRICAL_SURFACE ( 'NONE', #11657, 1.000000000000000888 ) ;
#6671=CARTESIAN_POINT ( 'NONE',  ( -15.00000000000000000, 316.7545334744432353, 495.1946179577816451 ) ) ;
#6695=( NAMED_UNIT ( * ) PLANE_ANGLE_UNIT ( ) SI_UNIT ( $, .RADIAN. ) );
#6698=CARTESIAN_POINT ( 'NONE',  ( -15.00000000000000000, 317.7545334744432353, 495.1946179577816451 ) ) ;
#6720=DIRECTION ( 'NONE',  ( 3.392348130799086764E-14, 0.000000000000000000, -1.000000000000000000 ) ) ;
#6723=CARTESIAN_POINT ( 'NONE',  ( -78.99999999999995737, 141.3905724437643414, 503.0282008302663144 ) ) ;
#6729=EDGE_CURVE ( 'NONE', #4741, #1482, #8332, .T. ) ;
#6730=CARTESIAN_POINT ( 'NONE',  ( -15.00000000000000000, 317.7545334744432353, 495.1946179577816451 ) ) ;
#6742=PLANE ( 'NONE',  #19248 ) ;
#6747=CARTESIAN_POINT ( 'NONE',  ( -1.000000000000000888, 216.7545334744432921, 477.3411705753777596 ) ) ;
#6766=VECTOR ( 'NONE', #6319, 1000.000000000000000 ) ;
#6768=ORIENTED_EDGE ( 'NONE', *, *, #11088, .T. ) ;
#6778=CIRCLE ( 'NONE', #4737, 8.000000000000007105 ) ;
#6782=DIRECTION ( 'NONE',  ( 0.000000000000000000, 0.000000000000000000, -1.000000000000000000 ) ) ;
#6784=DIRECTION ( 'NONE',  ( 0.000000000000000000, 1.000000000000000000, 0.000000000000000000 ) ) ;
#6788=CIRCLE ( 'NONE', #180, 3.883636366625808911 ) ;
#6794=VECTOR ( 'NONE', #18383, 1000.000000000000000 ) ;
#6797=DIRECTION ( 'NONE',  ( 0.000000000000000000, -0.9497703099767278445, -0.3129478523439812032 ) ) ;
#6798=ORIENTED_EDGE ( 'NONE', *, *, #4440, .T. ) ;
#6801=EDGE_CURVE ( 'NONE', #9471, #3904, #10166, .T. ) ;
#6805=CARTESIAN_POINT ( 'NONE',  ( 0.02413213198956416089, 140.0034334293438292, 488.8196209980684444 ) ) ;
#6819=VECTOR ( 'NONE', #19454, 1000.000000000000000 ) ;
#6826=FILL_AREA_STYLE ('',( #15045 ) ) ;
#6831=CARTESIAN_POINT ( 'NONE',  ( -79.99999999999995737, 146.8256012863087676, 480.6843163258853906 ) ) ;
#6839=AXIS2_PLACEMENT_3D ( 'NONE', #19964, #5968, #4421 ) ;
#6841=ORIENTED_EDGE ( 'NONE', *, *, #8989, .F. ) ;
#6845=UNCERTAINTY_MEASURE_WITH_UNIT (LENGTH_MEASURE( 1.000000000000000082E-05 ), #7124, 'distance_accuracy_value', 'NONE');
#6866=CARTESIAN_POINT ( 'NONE',  ( -1.000000000000000888, 138.7545334744432637, 510.3921618609452935 ) ) ;
#6868=VERTEX_POINT ( 'NONE', #17066 ) ;
#6876=DIRECTION ( 'NONE',  ( 0.000000000000000000, 0.000000000000000000, 1.000000000000000000 ) ) ;
#6882=DIRECTION ( 'NONE',  ( -0.000000000000000000, -0.000000000000000000, 1.000000000000000000 ) ) ;
#6885=EDGE_CURVE ( 'NONE', #15750, #17405, #14148, .T. ) ;
#6892=EDGE_CURVE ( 'NONE', #11867, #18810, #16802, .T. ) ;
#6896=ORIENTED_EDGE ( 'NONE', *, *, #14628, .T. ) ;
#6899=CARTESIAN_POINT ( 'NONE',  ( 0.7372031773519938103, 138.7723821178321657, 490.5025619606645364 ) ) ;
#6901=DIRECTION ( 'NONE',  ( 0.000000000000000000, 0.000000000000000000, 1.000000000000000000 ) ) ;
#6902=AXIS2_PLACEMENT_3D ( 'NONE', #19699, #14780, #10057 ) ;
#6904=( NAMED_UNIT ( * ) SI_UNIT ( $, .STERADIAN. ) SOLID_ANGLE_UNIT ( ) );
#6909=ORIENTED_EDGE ( 'NONE', *, *, #12936, .F. ) ;
#6923=CARTESIAN_POINT ( 'NONE',  ( -15.00000000000000000, 317.7545334744432353, 495.1946179577816451 ) ) ;
#6929=LINE ( 'NONE', #6723, #5304 ) ;
#6938=AXIS2_PLACEMENT_3D ( 'NONE', #1449, #3004, #9498 ) ;
#6957=CARTESIAN_POINT ( 'NONE',  ( -81.18192946989275072, 140.4048636633015406, 499.8237260975782874 ) ) ;
#6977=VECTOR ( 'NONE', #5324, 1000.000000000000000 ) ;
#6980=ORIENTED_EDGE ( 'NONE', *, *, #16821, .F. ) ;
#6987=CARTESIAN_POINT ( 'NONE',  ( 2.181929469892510465, 138.7545334744432637, 490.5655098179832976 ) ) ;
#7008=MECHANICAL_DESIGN_GEOMETRIC_PRESENTATION_REPRESENTATION('',(#15894),#18166);
#7012=MECHANICAL_DESIGN_GEOMETRIC_PRESENTATION_REPRESENTATION('',(#5373),#6006);
#7014=ORIENTED_EDGE ( 'NONE', *, *, #13666, .F. ) ;
#7022=VECTOR ( 'NONE', #13337, 1000.000000000000000 ) ;
#7025=ADVANCED_FACE ( 'NONE', ( #18015 ), #8851, .F. ) ;
#7042=UNCERTAINTY_MEASURE_WITH_UNIT (LENGTH_MEASURE( 1.000000000000000082E-05 ), #15339, 'distance_accuracy_value', 'NONE');
#7047=CARTESIAN_POINT ( 'NONE',  ( 1.000000000001310063, 216.7545334744432921, 489.5655098179835818 ) ) ;
#7058=ORIENTED_EDGE ( 'NONE', *, *, #19672, .T. ) ;
#7082=ORIENTED_EDGE ( 'NONE', *, *, #1287, .T. ) ;
#7085=CIRCLE ( 'NONE', #17921, 0.9999999999999974465 ) ;
#7086=ORIENTED_EDGE ( 'NONE', *, *, #317, .F. ) ;
#7095=LINE ( 'NONE', #3682, #2448 ) ;
#7102=CARTESIAN_POINT ( 'NONE',  ( -0.5185395424450671698, 138.8549385558393681, 489.7242651416971739 ) ) ;
#7104=CYLINDRICAL_SURFACE ( 'NONE', #4869, 1.000000000000000888 ) ;
#7105=CARTESIAN_POINT ( 'NONE',  ( -58.16843972078500258, 317.7545334744432353, 489.0536462814662286 ) ) ;
#7115=ORIENTED_EDGE ( 'NONE', *, *, #6892, .T. ) ;
#7118=AXIS2_PLACEMENT_3D ( 'NONE', #13227, #18247, #19473 ) ;
#7120=CARTESIAN_POINT ( 'NONE',  ( -21.85283368562565443, 319.7545334744432353, 481.2863735482146694 ) ) ;
#7123=EDGE_CURVE ( 'NONE', #13692, #6152, #4223, .T. ) ;
#7124=( LENGTH_UNIT ( ) NAMED_UNIT ( * ) SI_UNIT ( .MILLI., .METRE. ) );
#7125=CARTESIAN_POINT ( 'NONE',  ( -78.99999999999995737, 138.3494706343262237, 489.1604469778678776 ) ) ;
#7133=CARTESIAN_POINT ( 'NONE',  ( 2.181929469892549545, 147.7545334744432921, 491.0690926367355473 ) ) ;
#7135=VECTOR ( 'NONE', #19358, 1000.000000000000000 ) ;
#7149=DIRECTION ( 'NONE',  ( 1.000000000000000000, 0.000000000000000000, 1.322948291343119651E-12 ) ) ;
#7150=DIRECTION ( 'NONE',  ( 1.445602896647347002E-15, 0.000000000000000000, 1.000000000000000000 ) ) ;
#7153=FACE_OUTER_BOUND ( 'NONE', #6149, .T. ) ;
#7155=CARTESIAN_POINT ( 'NONE',  ( -79.99999999999995737, 138.7545334744432637, 477.3411705753777596 ) ) ;
#7165=ORIENTED_EDGE ( 'NONE', *, *, #11486, .F. ) ;
#7167=CARTESIAN_POINT ( 'NONE',  ( -79.99999999999995737, 316.7545334744432353, 495.1946179577816451 ) ) ;
#7171=CARTESIAN_POINT ( 'NONE',  ( -78.99999999999995737, 140.6767260202136072, 502.2320488918456931 ) ) ;
#7189=ORIENTED_EDGE ( 'NONE', *, *, #196, .F. ) ;
#7192=SURFACE_SIDE_STYLE ('',( #18300 ) ) ;
#7195=CARTESIAN_POINT ( 'NONE',  ( -58.16843972078500258, 319.7545334744432353, 489.0536462814662286 ) ) ;
#7230=CARTESIAN_POINT ( 'NONE',  ( -1.994931997373328159E-14, 147.7545334744432921, 496.6642397995874489 ) ) ;
#7245=CARTESIAN_POINT ( 'NONE',  ( -80.73480563767387252, 139.7732851794904434, 489.5387775887227235 ) ) ;
#7248=ORIENTED_EDGE ( 'NONE', *, *, #13696, .F. ) ;
#7252=AXIS2_PLACEMENT_3D ( 'NONE', #5934, #19933, #7391 ) ;
#7268=CARTESIAN_POINT ( 'NONE',  ( -1.000000000000000888, 216.7545334744432921, 509.3921618609452935 ) ) ;
#7270=MECHANICAL_DESIGN_GEOMETRIC_PRESENTATION_REPRESENTATION('',(#4631),#9898);
#7292=CARTESIAN_POINT ( 'NONE',  ( -44.50085094405410757, 209.4098724938429541, 505.3921618609452935 ) ) ;
#7293=FACE_OUTER_BOUND ( 'NONE', #9321, .T. ) ;
#7294=DIRECTION ( 'NONE',  ( -0.000000000000000000, 0.7071067811865504593, -0.7071067811865445751 ) ) ;
#7295=( LENGTH_UNIT ( ) NAMED_UNIT ( * ) SI_UNIT ( .MILLI., .METRE. ) );
#7301=EDGE_LOOP ( 'NONE', ( #8124, #4775, #2899, #10115, #18594, #5625 ) ) ;
#7305=CARTESIAN_POINT ( 'NONE',  ( -21.85283368562565443, 319.7545334744432353, 485.1700099148404774 ) ) ;
#7311=CARTESIAN_POINT ( 'NONE',  ( -81.18192946987610981, 139.7545334744432637, -2.701928103162370948E-12 ) ) ;
#7312=LINE ( 'NONE', #15455, #17649 ) ;
#7314=PLANE ( 'NONE',  #6839 ) ;
#7342=CARTESIAN_POINT ( 'NONE',  ( -79.98710143421158136, 138.7963597474245603, 490.1983628228959446 ) ) ;
#7345=AXIS2_PLACEMENT_3D ( 'NONE', #18755, #2684, #14119 ) ;
#7358=LINE ( 'NONE', #649, #7890 ) ;
#7369=CARTESIAN_POINT ( 'NONE',  ( -1.000000000000013545, 138.3494706343262237, 489.1604469778678776 ) ) ;
#7391=DIRECTION ( 'NONE',  ( 0.000000000000000000, 0.9980168174369414835, 0.06294785233063035501 ) ) ;
#7399=CARTESIAN_POINT ( 'NONE',  ( -41.50085094405408626, 209.4098724938429541, 505.3921618609452935 ) ) ;
#7405=CARTESIAN_POINT ( 'NONE',  ( -58.16843972078500258, 319.7545334744432353, 489.0536462814662286 ) ) ;
#7408=COLOUR_RGB ( '', 0.09019608, 0.27058824, 0.51372549) ;
#7413=ORIENTED_EDGE ( 'NONE', *, *, #5148, .F. ) ;
#7415=ORIENTED_EDGE ( 'NONE', *, *, #1812, .F. ) ;
#7417=CARTESIAN_POINT ( 'NONE',  ( -78.99999999999995737, 138.7545334744432637, 477.3411705753777596 ) ) ;
#7421=AXIS2_PLACEMENT_3D ( 'NONE', #3962, #16545, #3567 ) ;
#7439=AXIS2_PLACEMENT_3D ( 'NONE', #8575, #17963, #3945 ) ;
#7442=EDGE_LOOP ( 'NONE', ( #9884, #6098, #19348, #12598 ) ) ;
#7447=CARTESIAN_POINT ( 'NONE',  ( -1.000000000000008216, 144.4616402556298453, 504.6850550797586834 ) ) ;
#7455=DIRECTION ( 'NONE',  ( 0.000000000000000000, 0.000000000000000000, -1.000000000000000000 ) ) ;
#7457=CARTESIAN_POINT ( 'NONE',  ( -80.12162488254176651, 138.9594563584317086, 489.0814894912512045 ) ) ;
#7470=TOROIDAL_SURFACE ( 'NONE', #9761, 8.000000000000000000, 1.000000000000000000 ) ;
#7474=( NAMED_UNIT ( * ) PLANE_ANGLE_UNIT ( ) SI_UNIT ( $, .RADIAN. ) );
#7489=ORIENTED_EDGE ( 'NONE', *, *, #15818, .F. ) ;
#7509=ADVANCED_FACE ( 'NONE', ( #15480 ), #2783, .T. ) ;
#7510=ORIENTED_EDGE ( 'NONE', *, *, #19672, .F. ) ;
#7511=ORIENTED_EDGE ( 'NONE', *, *, #10523, .T. ) ;
#7515=CARTESIAN_POINT ( 'NONE',  ( -21.85283368562565443, 319.7545334744432353, 485.1700099148404774 ) ) ;
#7526=ADVANCED_FACE ( 'NONE', ( #9172 ), #17023, .T. ) ;
#7529=EDGE_LOOP ( 'NONE', ( #7115, #17553, #12867, #18600 ) ) ;
#7538=CARTESIAN_POINT ( 'NONE',  ( -82.18192946989263703, 139.7545334744432637, 496.6642397995873921 ) ) ;
#7546=VERTEX_POINT ( 'NONE', #17104 ) ;
#7547=VECTOR ( 'NONE', #19610, 1000.000000000000000 ) ;
#7561=CARTESIAN_POINT ( 'NONE',  ( -78.99999999999995737, 216.7545334744432921, 478.3411705753777596 ) ) ;
#7573=ORIENTED_EDGE ( 'NONE', *, *, #16350, .F. ) ;
#7599=PRODUCT ( 'Part12^Assem2', 'Part12^Assem2', '', ( #5830 ) ) ;
#7603=FACE_OUTER_BOUND ( 'NONE', #771, .T. ) ;
#7611=EDGE_CURVE ( 'NONE', #19713, #18686, #20084, .T. ) ;
#7623=ORIENTED_EDGE ( 'NONE', *, *, #4793, .F. ) ;
#7624=ORIENTED_EDGE ( 'NONE', *, *, #9503, .F. ) ;
#7625=EDGE_CURVE ( 'NONE', #19819, #3908, #2578, .T. ) ;
#7634=DIRECTION ( 'NONE',  ( 1.000000000000000000, -0.000000000000000000, -0.000000000000000000 ) ) ;
#7639=MECHANICAL_DESIGN_GEOMETRIC_PRESENTATION_REPRESENTATION('',(#17176),#17839);
#7641=DIRECTION ( 'NONE',  ( -0.000000000000000000, -1.000000000000000000, -0.000000000000000000 ) ) ;
#7643=ORIENTED_EDGE ( 'NONE', *, *, #5848, .F. ) ;
#7644=DIRECTION ( 'NONE',  ( -1.000000000000000000, 0.000000000000000000, 0.000000000000000000 ) ) ;
#7656=ORIENTED_EDGE ( 'NONE', *, *, #16009, .T. ) ;
#7661=AXIS2_PLACEMENT_3D ( 'NONE', #1888, #12957, #9843 ) ;
#7671=MECHANICAL_DESIGN_GEOMETRIC_PRESENTATION_REPRESENTATION('',(#16889),#17871);
#7673=ORIENTED_EDGE ( 'NONE', *, *, #17310, .T. ) ;
#7674=FACE_OUTER_BOUND ( 'NONE', #147, .T. ) ;
#7676=VERTEX_POINT ( 'NONE', #7538 ) ;
#7682=VECTOR ( 'NONE', #3971, 1000.000000000000000 ) ;
#7689=EDGE_CURVE ( 'NONE', #12429, #566, #9924, .T. ) ;
#7709=DIRECTION ( 'NONE',  ( 0.000000000000000000, 0.000000000000000000, -1.000000000000000000 ) ) ;
#7715=COLOUR_RGB ( '', 0.09019608, 0.27058824, 0.51372549) ;
#7733=AXIS2_PLACEMENT_3D ( 'NONE', #20137, #6046, #15747 ) ;
#7739=COLOUR_RGB ( '', 0.08235294, 0.09019608, 0.10196078) ;
#7743=SURFACE_STYLE_USAGE ( .BOTH. , #9087 ) ;
#7745=ORIENTED_EDGE ( 'NONE', *, *, #11745, .F. ) ;
#7769=CARTESIAN_POINT ( 'NONE',  ( -81.18192946989242387, 216.7545334744432921, 490.5655098179833544 ) ) ;
#7772=SURFACE_STYLE_FILL_AREA ( #9195 ) ;
#7774=CARTESIAN_POINT ( 'NONE',  ( 0.8562747324767706614, 140.4115240776867495, 500.8315376115346567 ) ) ;
#7779=DIRECTION ( 'NONE',  ( 0.000000000000000000, 0.000000000000000000, 1.000000000000000000 ) ) ;
#7794=EDGE_CURVE ( 'NONE', #9566, #13692, #3516, .T. ) ;
#7796=CARTESIAN_POINT ( 'NONE',  ( -80.10887714076795874, 139.9048413501793391, 489.0362475460869973 ) ) ;
#7800=ORIENTED_EDGE ( 'NONE', *, *, #12255, .F. ) ;
#7808=ORIENTED_EDGE ( 'NONE', *, *, #1925, .T. ) ;
#7813=CARTESIAN_POINT ( 'NONE',  ( 0.000000000000000000, 0.000000000000000000, 495.1946179577816451 ) ) ;
#7817=EDGE_LOOP ( 'NONE', ( #17943, #18481, #2415, #17382 ) ) ;
#7821=( NAMED_UNIT ( * ) SI_UNIT ( $, .STERADIAN. ) SOLID_ANGLE_UNIT ( ) );
#7835=CYLINDRICAL_SURFACE ( 'NONE', #3772, 3.883636366625808911 ) ;
#7841=FILL_AREA_STYLE_COLOUR ( '', #12667 ) ;
#7843=( NAMED_UNIT ( * ) PLANE_ANGLE_UNIT ( ) SI_UNIT ( $, .RADIAN. ) );
#7861=CARTESIAN_POINT ( 'NONE',  ( 0.8155011883608258572, 139.7530151083513772, 500.8359591266525968 ) ) ;
#7867=CARTESIAN_POINT ( 'NONE',  ( -81.18192946989275072, 216.7545334744432921, 500.8237260975782874 ) ) ;
#7869=FILL_AREA_STYLE ('',( #18685 ) ) ;
#7873=EDGE_CURVE ( 'NONE', #18411, #19036, #3710, .T. ) ;
#7876=AXIS2_PLACEMENT_3D ( 'NONE', #7311, #15246, #13703 ) ;
#7880=ADVANCED_FACE ( 'NONE', ( #13113 ), #11639, .T. ) ;
#7890=VECTOR ( 'NONE', #5511, 1000.000000000000114 ) ;
#7891=LINE ( 'NONE', #4389, #10664 ) ;
#7892=ORIENTED_EDGE ( 'NONE', *, *, #5725, .F. ) ;
#7910=CARTESIAN_POINT ( 'NONE',  ( -79.34077595268365712, 139.9822134344571225, 501.2042671826797573 ) ) ;
#7912=CARTESIAN_POINT ( 'NONE',  ( -79.99999999999995737, 138.7545334744432637, 489.5655098179848892 ) ) ;
#7914=ORIENTED_EDGE ( 'NONE', *, *, #17944, .F. ) ;
#7915=CARTESIAN_POINT ( 'NONE',  ( -64.99999999999995737, 317.7545334744432353, 495.1946179577816451 ) ) ;
#7918=LINE ( 'NONE', #14309, #8484 ) ;
#7938=CARTESIAN_POINT ( 'NONE',  ( -1.000000000000007550, 146.8256012863087676, 480.6843163258854474 ) ) ;
#7944=DIRECTION ( 'NONE',  ( 0.000000000000000000, 0.000000000000000000, -1.000000000000000000 ) ) ;
#7947=CARTESIAN_POINT ( 'NONE',  ( -81.18192946989243808, 138.7723821175108014, 490.5025619657601510 ) ) ;
#7949=VECTOR ( 'NONE', #5783, 1000.000000000000000 ) ;
#7958=ORIENTED_EDGE ( 'NONE', *, *, #12033, .F. ) ;
#7959=DIRECTION ( 'NONE',  ( -0.000000000000000000, -0.000000000000000000, 1.000000000000000000 ) ) ;
#7962=CARTESIAN_POINT ( 'NONE',  ( -0.7871933770022689902, 140.1302042697082300, 501.4486251228268543 ) ) ;
#7963=DIRECTION ( 'NONE',  ( 1.000000000000000000, 0.000000000000000000, 1.135258727068399668E-15 ) ) ;
#7966=VECTOR ( 'NONE', #1599, 1000.000000000000000 ) ;
#7967=ORIENTED_EDGE ( 'NONE', *, *, #6657, .T. ) ;
#7972=ORIENTED_EDGE ( 'NONE', *, *, #4171, .F. ) ;
#7979=ORIENTED_EDGE ( 'NONE', *, *, #13931, .F. ) ;
#7985=ORIENTED_EDGE ( 'NONE', *, *, #8535, .F. ) ;
#7986=EDGE_CURVE ( 'NONE', #15133, #18411, #766, .T. ) ;
#7989=CIRCLE ( 'NONE', #9982, 1.000000000000015987 ) ;
#7992=CARTESIAN_POINT ( 'NONE',  ( -78.99999999999995737, 147.7545334744432921, 496.6642397995874489 ) ) ;
#7994=VECTOR ( 'NONE', #5315, 1000.000000000000000 ) ;
#8004=DIRECTION ( 'NONE',  ( 1.000000000000000000, 8.344193210541727648E-14, -1.322943490866811299E-12 ) ) ;
#8019=ORIENTED_EDGE ( 'NONE', *, *, #12147, .T. ) ;
#8021=LINE ( 'NONE', #14501, #7966 ) ;
#8022=DIRECTION ( 'NONE',  ( -0.000000000000000000, -0.000000000000000000, 1.000000000000000000 ) ) ;
#8027=CARTESIAN_POINT ( 'NONE',  ( -1.000000000000000888, 146.1184945051221575, 507.7561228916242158 ) ) ;
#8029=DIRECTION ( 'NONE',  ( -1.000000000000000000, -0.000000000000000000, -1.135258727068399668E-15 ) ) ;
#8034=EDGE_LOOP ( 'NONE', ( #11353, #6585, #17476, #1324 ) ) ;
#8049=DIRECTION ( 'NONE',  ( -0.000000000000000000, -0.7071067811865445751, -0.7071067811865504593 ) ) ;
#8061=AXIS2_PLACEMENT_3D ( 'NONE', #7133, #8259, #13122 ) ;
#8067=ADVANCED_FACE ( 'NONE', ( #12553 ), #18816, .F. ) ;
#8076=CARTESIAN_POINT ( 'NONE',  ( -0.08067209305391118135, 139.6450463499541570, 500.5689801128370391 ) ) ;
#8078=AXIS2_PLACEMENT_3D ( 'NONE', #17041, #13740, #10545 ) ;
#8080=CYLINDRICAL_SURFACE ( 'NONE', #12526, 1.000000000000000888 ) ;
#8090=VERTEX_POINT ( 'NONE', #9457 ) ;
#8094=TOROIDAL_SURFACE ( 'NONE', #5463, 8.000000000000000000, 1.000000000000000000 ) ;
#8105=FACE_BOUND ( 'NONE', #9565, .T. ) ;
#8107=CARTESIAN_POINT ( 'NONE',  ( 1.181929469893224560, 140.4048636633015406, 499.8237260975781737 ) ) ;
#8116=DIRECTION ( 'NONE',  ( -0.000000000000000000, 1.000000000000000000, -0.000000000000000000 ) ) ;
#8121=FACE_OUTER_BOUND ( 'NONE', #4056, .T. ) ;
#8124=ORIENTED_EDGE ( 'NONE', *, *, #1295, .T. ) ;
#8135=MANIFOLD_SOLID_BREP ( 'Cut-Extrude2', #3401 ) ;
#8138=DIRECTION ( 'NONE',  ( -0.000000000000000000, 1.000000000000000000, -0.000000000000000000 ) ) ;
#8146=EDGE_CURVE ( 'NONE', #1021, #13927, #4021, .T. ) ;
#8148=ORIENTED_EDGE ( 'NONE', *, *, #16934, .F. ) ;
#8149=UNCERTAINTY_MEASURE_WITH_UNIT (LENGTH_MEASURE( 1.000000000000000082E-05 ), #16682, 'distance_accuracy_value', 'NONE');
#8154=DIRECTION ( 'NONE',  ( 1.000000000000000000, -0.000000000000000000, -1.450371633464475582E-15 ) ) ;
#8167=EDGE_CURVE ( 'NONE', #19489, #5765, #19522, .T. ) ;
#8169=EDGE_CURVE ( 'NONE', #8090, #17153, #1691, .T. ) ;
#8171=AXIS2_PLACEMENT_3D ( 'NONE', #11520, #19530, #2435 ) ;
#8176=LINE ( 'NONE', #11245, #6766 ) ;
#8182=CARTESIAN_POINT ( 'NONE',  ( -1.000000000000009104, 141.3905724437643698, 484.7051316060566819 ) ) ;
#8188=ORIENTED_EDGE ( 'NONE', *, *, #15822, .T. ) ;
#8193=ORIENTED_EDGE ( 'NONE', *, *, #11019, .F. ) ;
#8219=CARTESIAN_POINT ( 'NONE',  ( -80.10586188290847076, 140.9786807048501487, 501.3714379820334557 ) ) ;
#8221=ORIENTED_EDGE ( 'NONE', *, *, #10412, .T. ) ;
#8223=CARTESIAN_POINT ( 'NONE',  ( 1.181929469893224560, 140.4048636633015406, 499.8237260975782874 ) ) ;
#8226=ORIENTED_EDGE ( 'NONE', *, *, #14393, .T. ) ;
#8229=LINE ( 'NONE', #6280, #13582 ) ;
#8230=MANIFOLD_SOLID_BREP ( 'Fillet4', #2065 ) ;
#8233=PLANE ( 'NONE',  #10135 ) ;
#8234=DIRECTION ( 'NONE',  ( 1.000000000000000000, 0.000000000000000000, 0.000000000000000000 ) ) ;
#8236=CARTESIAN_POINT ( 'NONE',  ( -79.99999999999995737, 141.6406393683236331, 501.8237260975782874 ) ) ;
#8237=LINE ( 'NONE', #6698, #14845 ) ;
#8251=DIRECTION ( 'NONE',  ( 0.000000000000000000, -0.000000000000000000, -1.000000000000000000 ) ) ;
#8253=CYLINDRICAL_SURFACE ( 'NONE', #13282, 1.000000000000015987 ) ;
#8259=DIRECTION ( 'NONE',  ( 1.000000000000000000, -0.000000000000000000, -7.715811803773179210E-14 ) ) ;
#8266=DIRECTION ( 'NONE',  ( 0.000000000000000000, 0.9187087263927379288, -0.3949357872488051813 ) ) ;
#8271=VERTEX_POINT ( 'NONE', #17064 ) ;
#8278=DIRECTION ( 'NONE',  ( -0.000000000000000000, -0.000000000000000000, 1.000000000000000000 ) ) ;
#8284=FACE_OUTER_BOUND ( 'NONE', #14562, .T. ) ;
#8297=CIRCLE ( 'NONE', #10584, 3.883636366625808911 ) ;
#8302=CARTESIAN_POINT ( 'NONE',  ( -41.50085094405408626, 193.0431417881923153, 505.3921618609452935 ) ) ;
#8303=ORIENTED_EDGE ( 'NONE', *, *, #1635, .F. ) ;
#8306=DIRECTION ( 'NONE',  ( 0.000000000000000000, 0.000000000000000000, 1.000000000000000000 ) ) ;
#8308=CARTESIAN_POINT ( 'NONE',  ( 0.000000000000000000, 216.7545334744432921, 495.1946179577816451 ) ) ;
#8316=ORIENTED_EDGE ( 'NONE', *, *, #15822, .F. ) ;
#8317=CARTESIAN_POINT ( 'NONE',  ( -1.387778780781445676E-14, 216.7545334744432921, 489.5655098179848892 ) ) ;
#8325=CARTESIAN_POINT ( 'NONE',  ( -79.91454752859293365, 140.3642491793935676, 501.8091283190183844 ) ) ;
#8332=LINE ( 'NONE', #19338, #14479 ) ;
#8333=CARTESIAN_POINT ( 'NONE',  ( 2.181929469893224560, 216.7545334744432921, 499.8237260975781169 ) ) ;
#8340=VERTEX_POINT ( 'NONE', #12745 ) ;
#8345=TOROIDAL_SURFACE ( 'NONE', #2052, 8.000000000000000000, 1.000000000000000000 ) ;
#8360=DIRECTION ( 'NONE',  ( -0.000000000000000000, -0.7071067811865455743, -0.7071067811865493491 ) ) ;
#8371=ORIENTED_EDGE ( 'NONE', *, *, #6801, .T. ) ;
#8387=FACE_OUTER_BOUND ( 'NONE', #12569, .T. ) ;
#8390=DIRECTION ( 'NONE',  ( 0.000000000000000000, 0.9980168174361081501, 0.06294785234384196737 ) ) ;
#8395=( NAMED_UNIT ( * ) SI_UNIT ( $, .STERADIAN. ) SOLID_ANGLE_UNIT ( ) );
#8399=ORIENTED_EDGE ( 'NONE', *, *, #667, .F. ) ;
#8403=ORIENTED_EDGE ( 'NONE', *, *, #9922, .F. ) ;
#8416=FILL_AREA_STYLE_COLOUR ( '', #10628 ) ;
#8423=AXIS2_PLACEMENT_3D ( 'NONE', #3131, #12412, #18678 ) ;
#8431=EDGE_CURVE ( 'NONE', #2341, #1465, #11392, .T. ) ;
#8432=ORIENTED_EDGE ( 'NONE', *, *, #12033, .T. ) ;
#8437=CARTESIAN_POINT ( 'NONE',  ( 1.181929469892950335, 147.7545334744432921, 496.6642397995874489 ) ) ;
#8441=CARTESIAN_POINT ( 'NONE',  ( 0.7345891654137221005, 139.7733146779539481, 489.5386252392920028 ) ) ;
#8443=DIRECTION ( 'NONE',  ( 0.000000000000000000, 0.000000000000000000, -1.000000000000000000 ) ) ;
#8477=CARTESIAN_POINT ( 'NONE',  ( -78.99999999999995737, 152.4824555358010798, 510.3921618609452935 ) ) ;
#8478=DIRECTION ( 'NONE',  ( 0.000000000000000000, -0.7071067811865753283, -0.7071067811865198172 ) ) ;
#8479=ADVANCED_FACE ( 'NONE', ( #18158 ), #13276, .T. ) ;
#8484=VECTOR ( 'NONE', #6589, 1000.000000000000000 ) ;
#8486=VERTEX_POINT ( 'NONE', #11801 ) ;
#8499=FACE_OUTER_BOUND ( 'NONE', #9290, .T. ) ;
#8503=CARTESIAN_POINT ( 'NONE',  ( -79.38892094406317312, 138.8697078648616525, 489.6181569159061837 ) ) ;
#8508=ADVANCED_FACE ( 'NONE', ( #4713 ), #9242, .F. ) ;
#8533=EDGE_LOOP ( 'NONE', ( #11582, #11150, #16723, #17556, #11710, #4216, #19447, #18430, #9886, #4221 ) ) ;
#8535=EDGE_CURVE ( 'NONE', #17405, #19090, #11581, .T. ) ;
#8543=AXIS2_PLACEMENT_3D ( 'NONE', #19734, #12052, #13689 ) ;
#8546=LINE ( 'NONE', #14434, #2321 ) ;
#8553=ORIENTED_EDGE ( 'NONE', *, *, #11511, .T. ) ;
#8560=EDGE_LOOP ( 'NONE', ( #7165, #5452, #7415, #2724 ) ) ;
#8563=DIRECTION ( 'NONE',  ( 0.000000000000000000, -0.7071067811865336949, -0.7071067811865614505 ) ) ;
#8575=CARTESIAN_POINT ( 'NONE',  ( -21.85283368562565443, 319.7545334744432353, 485.1700099148404774 ) ) ;
#8591=EDGE_CURVE ( 'NONE', #18058, #506, #8297, .T. ) ;
#8596=LINE ( 'NONE', #16551, #4965 ) ;
#8601=CARTESIAN_POINT ( 'NONE',  ( -78.99999999999995737, 146.1184945051222428, 479.9772095446988374 ) ) ;
#8619=CARTESIAN_POINT ( 'NONE',  ( -0.03866188257987528132, 139.1517308181911403, 488.4190873714470058 ) ) ;
#8624=DIRECTION ( 'NONE',  ( 1.000000000000000000, 0.000000000000000000, 0.000000000000000000 ) ) ;
#8627=VECTOR ( 'NONE', #13570, 1000.000000000000000 ) ;
#8631=EDGE_CURVE ( 'NONE', #4888, #15103, #14396, .T. ) ;
#8632=AXIS2_PLACEMENT_3D ( 'NONE', #16453, #2301, #16368 ) ;
#8650=FILL_AREA_STYLE ('',( #2240 ) ) ;
#8653=DIRECTION ( 'NONE',  ( 1.000000000000000000, 0.000000000000000000, 0.000000000000000000 ) ) ;
#8656=CARTESIAN_POINT ( 'NONE',  ( 0.000000000000000000, 140.4048636633015406, 499.8237260975782874 ) ) ;
#8677=CARTESIAN_POINT ( 'NONE',  ( -79.99999999999995737, 216.7545334744432921, 495.1946179577816451 ) ) ;
#8701=UNCERTAINTY_MEASURE_WITH_UNIT (LENGTH_MEASURE( 1.000000000000000082E-05 ), #6096, 'distance_accuracy_value', 'NONE');
#8705=CARTESIAN_POINT ( 'NONE',  ( -79.99999999999995737, 147.7545334744432921, 491.0690926367356042 ) ) ;
#8715=DIRECTION ( 'NONE',  ( 0.000000000000000000, 0.000000000000000000, -1.000000000000000000 ) ) ;
#8720=AXIS2_PLACEMENT_3D ( 'NONE', #1766, #6535, #12823 ) ;
#8723=STYLED_ITEM ( 'NONE', ( #5043 ), #15275 ) ;
#8736=VECTOR ( 'NONE', #16478, 1000.000000000000000 ) ;
#8738=CARTESIAN_POINT ( 'NONE',  ( 0.4691783309273026004, 138.7756623317111462, 490.4420716635970052 ) ) ;
#8742=SURFACE_SIDE_STYLE ('',( #16878 ) ) ;
#8758=SURFACE_STYLE_FILL_AREA ( #2456 ) ;
#8762=ADVANCED_FACE ( 'NONE', ( #1323 ), #15606, .F. ) ;
#8772=CARTESIAN_POINT ( 'NONE',  ( -81.18192946989263703, 139.7545334744432637, 496.6642397995874489 ) ) ;
#8785=CARTESIAN_POINT ( 'NONE',  ( -1.000000000000001110, 216.7545334744432921, 478.3411705753777596 ) ) ;
#8787=DIRECTION ( 'NONE',  ( 0.000000000000000000, 0.000000000000000000, -1.000000000000000000 ) ) ;
#8805=PLANE ( 'NONE',  #310 ) ;
#8806=DIRECTION ( 'NONE',  ( 0.000000000000000000, 0.000000000000000000, -1.000000000000000000 ) ) ;
#8809=DIRECTION ( 'NONE',  ( -0.000000000000000000, 1.000000000000000000, -0.000000000000000000 ) ) ;
#8810=EDGE_CURVE ( 'NONE', #12373, #1145, #12208, .T. ) ;
#8813=ORIENTED_EDGE ( 'NONE', *, *, #5218, .F. ) ;
#8826=VERTEX_POINT ( 'NONE', #18484 ) ;
#8828=CARTESIAN_POINT ( 'NONE',  ( 0.01154096739894239568, 141.3438375788570909, 501.6399373741901968 ) ) ;
#8836=FILL_AREA_STYLE ('',( #18197 ) ) ;
#8851=CYLINDRICAL_SURFACE ( 'NONE', #14815, 1.000000000000000888 ) ;
#8859=EDGE_CURVE ( 'NONE', #10116, #16810, #2922, .T. ) ;
#8867=ORIENTED_EDGE ( 'NONE', *, *, #10523, .F. ) ;
#8874=FACE_OUTER_BOUND ( 'NONE', #7817, .T. ) ;
#8901=DIRECTION ( 'NONE',  ( 0.000000000000000000, 1.000000000000000000, 0.000000000000000000 ) ) ;
#8905=EDGE_LOOP ( 'NONE', ( #7248, #6664, #10766, #3108 ) ) ;
#8935=ORIENTED_EDGE ( 'NONE', *, *, #18347, .T. ) ;
#8937=EDGE_LOOP ( 'NONE', ( #3812, #18352, #15632, #13057 ) ) ;
#8942=FACE_OUTER_BOUND ( 'NONE', #8981, .T. ) ;
#8947=DIRECTION ( 'NONE',  ( 1.000000000000000000, 0.000000000000000000, 0.000000000000000000 ) ) ;
#8971=CARTESIAN_POINT ( 'NONE',  ( -78.99999999999995737, 152.4824555358011082, 486.3411705753778165 ) ) ;
#8973=ADVANCED_FACE ( 'NONE', ( #9018 ), #15321, .T. ) ;
#8975=DIRECTION ( 'NONE',  ( 0.000000000000000000, 0.000000000000000000, 1.000000000000000000 ) ) ;
#8977=CARTESIAN_POINT ( 'NONE',  ( -80.19446047282671941, 139.8569107142918995, 489.1724409064830184 ) ) ;
#8980=STYLED_ITEM ( 'NONE', ( #456 ), #3492 ) ;
#8981=EDGE_LOOP ( 'NONE', ( #175, #1178, #10096, #15291 ) ) ;
#8989=EDGE_CURVE ( 'NONE', #14850, #17220, #16348, .T. ) ;
#9003=CARTESIAN_POINT ( 'NONE',  ( 1.181929469893224560, 140.4048636633015406, 499.8237260975782874 ) ) ;
#9008=ORIENTED_EDGE ( 'NONE', *, *, #16533, .F. ) ;
#9016=MECHANICAL_DESIGN_GEOMETRIC_PRESENTATION_REPRESENTATION('',(#6059),#10665);
#9018=FACE_OUTER_BOUND ( 'NONE', #2755, .T. ) ;
#9021=CARTESIAN_POINT ( 'NONE',  ( 0.8260971242880760235, 140.4146325554252712, 500.8352231739891067 ) ) ;
#9022=ORIENTED_EDGE ( 'NONE', *, *, #19432, .F. ) ;
#9031=CARTESIAN_POINT ( 'NONE',  ( -78.99999999999995737, 146.1184945051222428, 479.9772095446988374 ) ) ;
#9033=AXIS2_PLACEMENT_3D ( 'NONE', #9440, #15749, #4694 ) ;
#9034=VECTOR ( 'NONE', #11654, 1000.000000000000000 ) ;
#9039=FACE_OUTER_BOUND ( 'NONE', #7442, .T. ) ;
#9048=ORIENTED_EDGE ( 'NONE', *, *, #4171, .T. ) ;
#9049=AXIS2_PLACEMENT_3D ( 'NONE', #20370, #2662, #6281 ) ;
#9051=ORIENTED_EDGE ( 'NONE', *, *, #14565, .F. ) ;
#9054=AXIS2_PLACEMENT_3D ( 'NONE', #4567, #9409, #19074 ) ;
#9057=CARTESIAN_POINT ( 'NONE',  ( 1.181929469891187301, 138.7545334744432637, 489.5655098179833544 ) ) ;
#9061=ORIENTED_EDGE ( 'NONE', *, *, #7123, .F. ) ;
#9078=ORIENTED_EDGE ( 'NONE', *, *, #4218, .T. ) ;
#9079=DIRECTION ( 'NONE',  ( 0.000000000000000000, -1.000000000000000000, 0.000000000000000000 ) ) ;
#9084=LINE ( 'NONE', #15374, #18863 ) ;
#9087=SURFACE_SIDE_STYLE ('',( #10825 ) ) ;
#9095=CARTESIAN_POINT ( 'NONE',  ( -80.10292611397925100, 138.7899753264051412, 490.2690555533860106 ) ) ;
#9109=CARTESIAN_POINT ( 'NONE',  ( -80.39206744217459288, 139.5296019426642147, 500.3183257186572064 ) ) ;
#9116=EDGE_CURVE ( 'NONE', #9147, #2723, #17259, .T. ) ;
#9147=VERTEX_POINT ( 'NONE', #19879 ) ;
#9151=EDGE_CURVE ( 'NONE', #17127, #15757, #20265, .T. ) ;
#9170=CARTESIAN_POINT ( 'NONE',  ( -1.000000000000000888, 216.7545334744432921, 510.3921618609452935 ) ) ;
#9172=FACE_OUTER_BOUND ( 'NONE', #1518, .T. ) ;
#9176=( NAMED_UNIT ( * ) SI_UNIT ( $, .STERADIAN. ) SOLID_ANGLE_UNIT ( ) );
#9177=FILL_AREA_STYLE ('',( #7841 ) ) ;
#9179=CARTESIAN_POINT ( 'NONE',  ( 0.9999999999997842837, 139.4861549369088323, 500.2186618848270996 ) ) ;
#9190=ORIENTED_EDGE ( 'NONE', *, *, #14538, .T. ) ;
#9195=FILL_AREA_STYLE ('',( #20319 ) ) ;
#9204=CIRCLE ( 'NONE', #8543, 1.000000000000000888 ) ;
#9217=CARTESIAN_POINT ( 'NONE',  ( 0.9116948254154977338, 140.4048636633015406, 500.8237260975782874 ) ) ;
#9223=CIRCLE ( 'NONE', #5567, 1.000000000000000888 ) ;
#9236=CIRCLE ( 'NONE', #10549, 3.000000000000002665 ) ;
#9242=PLANE ( 'NONE',  #12571 ) ;
#9243=VERTEX_POINT ( 'NONE', #5209 ) ;
#9245=EDGE_CURVE ( 'NONE', #10116, #11471, #1494, .T. ) ;
#9264=VERTEX_POINT ( 'NONE', #9170 ) ;
#9273=DIRECTION ( 'NONE',  ( 0.000000000000000000, 0.000000000000000000, 1.000000000000000000 ) ) ;
#9279=STYLED_ITEM ( 'NONE', ( #20035 ), #18050 ) ;
#9290=EDGE_LOOP ( 'NONE', ( #13448, #20078, #11462, #14391 ) ) ;
#9291=AXIS2_PLACEMENT_3D ( 'NONE', #15225, #786, #16586 ) ;
#9295=ORIENTED_EDGE ( 'NONE', *, *, #19712, .F. ) ;
#9301=FACE_OUTER_BOUND ( 'NONE', #5586, .T. ) ;
#9302=CIRCLE ( 'NONE', #3727, 3.000000000000009770 ) ;
#9304=CARTESIAN_POINT ( 'NONE',  ( -0.4029650338733730131, 139.7904024160982033, 500.8581393444502510 ) ) ;
#9306=DIRECTION ( 'NONE',  ( -0.000000000000000000, 1.000000000000000000, 0.000000000000000000 ) ) ;
#9310=PLANE ( 'NONE',  #15176 ) ;
#9314=ADVANCED_FACE ( 'NONE', ( #9384 ), #18540, .T. ) ;
#9318=ORIENTED_EDGE ( 'NONE', *, *, #6885, .F. ) ;
#9321=EDGE_LOOP ( 'NONE', ( #5861, #7958, #10067, #3608 ) ) ;
#9328=CARTESIAN_POINT ( 'NONE',  ( -80.36109718184712847, 139.8077570230245783, 489.3462760475625828 ) ) ;
#9337=CARTESIAN_POINT ( 'NONE',  ( -78.99999999999995737, 140.8764026050586722, 502.4686618848272133 ) ) ;
#9360=( GEOMETRIC_REPRESENTATION_CONTEXT ( 3 ) GLOBAL_UNCERTAINTY_ASSIGNED_CONTEXT ( ( #17740 ) ) GLOBAL_UNIT_ASSIGNED_CONTEXT ( ( #6357, #16981, #12638 ) ) REPRESENTATION_CONTEXT ( 'NONE', 'WORKASPACE' ) );
#9364=DIRECTION ( 'NONE',  ( -1.000000000000000000, -8.479266908829339085E-16, 0.000000000000000000 ) ) ;
#9365=CARTESIAN_POINT ( 'NONE',  ( -38.50085094405407204, 209.4098724938429541, 505.3921618609452935 ) ) ;
#9384=FACE_OUTER_BOUND ( 'NONE', #5430, .T. ) ;
#9386=AXIS2_PLACEMENT_3D ( 'NONE', #1950, #222, #8266 ) ;
#9389=( NAMED_UNIT ( * ) SI_UNIT ( $, .STERADIAN. ) SOLID_ANGLE_UNIT ( ) );
#9393=PLANE ( 'NONE',  #7345 ) ;
#9409=DIRECTION ( 'NONE',  ( 0.000000000000000000, -0.7071067811865455743, -0.7071067811865494601 ) ) ;
#9413=DIRECTION ( 'NONE',  ( -0.000000000000000000, -0.000000000000000000, 1.000000000000000000 ) ) ;
#9422=ORIENTED_EDGE ( 'NONE', *, *, #11008, .T. ) ;
#9423=( NAMED_UNIT ( * ) PLANE_ANGLE_UNIT ( ) SI_UNIT ( $, .RADIAN. ) );
#9426=COLOUR_RGB ( '', 0.08235294, 0.09019608, 0.10196078) ;
#9439=DIRECTION ( 'NONE',  ( 1.000000000000000000, 0.000000000000000000, 0.000000000000000000 ) ) ;
#9440=CARTESIAN_POINT ( 'NONE',  ( -21.85283368562565443, 317.7545334744432353, 485.1700099148404774 ) ) ;
#9444=CARTESIAN_POINT ( 'NONE',  ( -79.99999999999995737, 216.7545334744432921, 488.5655098179835818 ) ) ;
#9450=CIRCLE ( 'NONE', #1196, 1.000000000000000888 ) ;
#9453=CARTESIAN_POINT ( 'NONE',  ( -79.89735735534783601, 140.5749758762136423, 502.0985609692173739 ) ) ;
#9457=CARTESIAN_POINT ( 'NONE',  ( -80.99999999999995737, 216.7545334744432921, 500.8237260975782874 ) ) ;
#9464=AXIS2_PLACEMENT_3D ( 'NONE', #9873, #2014, #14100 ) ;
#9471=VERTEX_POINT ( 'NONE', #14216 ) ;
#9486=PRESENTATION_STYLE_ASSIGNMENT (( #4551 ) ) ;
#9492=ADVANCED_FACE ( 'NONE', ( #14521 ), #7470, .T. ) ;
#9494=EDGE_CURVE ( 'NONE', #10221, #1591, #5168, .T. ) ;
#9498=DIRECTION ( 'NONE',  ( 0.000000000000000000, 0.9187087263927379288, -0.3949357872488051813 ) ) ;
#9502=DIRECTION ( 'NONE',  ( -1.000000000000000000, -0.000000000000000000, 0.000000000000000000 ) ) ;
#9503=EDGE_CURVE ( 'NONE', #19125, #19958, #9887, .T. ) ;
#9504=AXIS2_PLACEMENT_3D ( 'NONE', #9003, #18372, #18472 ) ;
#9505=CARTESIAN_POINT ( 'NONE',  ( 0.5200485807784683834, 140.5123536700693876, 500.9436139292040480 ) ) ;
#9514=CARTESIAN_POINT ( 'NONE',  ( -1.000000000000014655, 152.4824555358010798, 501.3921618609452366 ) ) ;
#9519=CIRCLE ( 'NONE', #631, 9.000000000000007105 ) ;
#9522=VERTEX_POINT ( 'NONE', #11330 ) ;
#9526=CARTESIAN_POINT ( 'NONE',  ( -80.86158365502321033, 139.7703989349477069, 489.5655098179838092 ) ) ;
#9531=ORIENTED_EDGE ( 'NONE', *, *, #20299, .T. ) ;
#9533=DIRECTION ( 'NONE',  ( -0.000000000000000000, 1.000000000000000000, 0.000000000000000000 ) ) ;
#9537=LINE ( 'NONE', #6363, #19174 ) ;
#9538=B_SPLINE_CURVE_WITH_KNOTS ( 'NONE', 3,
 ( #12295, #13839, #16846, #10551, #4362, #11904, #18368, #5710, #20005, #20115, #15190, #12190 ),
 .UNSPECIFIED., .F., .F.,
 ( 4, 2, 2, 2, 2, 4 ),
 ( 0.000000000000000000, 0.0005192799409533858327, 0.001038559881906771665, 0.001557839822860157498, 0.001817479793336867436, 0.002077119763813577592 ),
 .UNSPECIFIED. ) ;
#9546=ORIENTED_EDGE ( 'NONE', *, *, #14778, .F. ) ;
#9565=EDGE_LOOP ( 'NONE', ( #1587, #6841, #5882, #15529 ) ) ;
#9566=VERTEX_POINT ( 'NONE', #13590 ) ;
#9570=VECTOR ( 'NONE', #16920, 1000.000000000000000 ) ;
#9581=DIRECTION ( 'NONE',  ( 0.000000000000000000, -0.7071067811865504593, 0.7071067811865445751 ) ) ;
#9586=VERTEX_POINT ( 'NONE', #4123 ) ;
#9589=ORIENTED_EDGE ( 'NONE', *, *, #17584, .F. ) ;
#9593=CARTESIAN_POINT ( 'NONE',  ( -82.18192946989275072, 216.7545334744432921, 499.8237260975782306 ) ) ;
#9594=STYLED_ITEM ( 'NONE', ( #3891 ), #8135 ) ;
#9595=ADVANCED_FACE ( 'NONE', ( #16705 ), #11749, .T. ) ;
#9599=FACE_OUTER_BOUND ( 'NONE', #3086, .T. ) ;
#9607=ORIENTED_EDGE ( 'NONE', *, *, #13216, .F. ) ;
#9608=SURFACE_STYLE_USAGE ( .BOTH. , #15731 ) ;
#9611=ORIENTED_EDGE ( 'NONE', *, *, #17584, .T. ) ;
#9614=ORIENTED_EDGE ( 'NONE', *, *, #19563, .T. ) ;
#9615=CARTESIAN_POINT ( 'NONE',  ( -64.99999999999995737, 317.7545334744432353, 495.1946179577816451 ) ) ;
#9616=DIRECTION ( 'NONE',  ( 0.000000000000000000, 0.000000000000000000, 1.000000000000000000 ) ) ;
#9618=EDGE_CURVE ( 'NONE', #14706, #368, #4896, .T. ) ;
#9643=STYLED_ITEM ( 'NONE', ( #16798 ), #170 ) ;
#9646=EDGE_CURVE ( 'NONE', #2022, #18268, #1082, .T. ) ;
#9652=CARTESIAN_POINT ( 'NONE',  ( -80.12128812903169717, 140.0129565146422124, 501.2795744101462674 ) ) ;
#9653=ORIENTED_EDGE ( 'NONE', *, *, #18375, .T. ) ;
#9655=CIRCLE ( 'NONE', #16581, 9.000000000000007105 ) ;
#9661=DIRECTION ( 'NONE',  ( -0.000000000000000000, 1.000000000000000000, 0.000000000000000000 ) ) ;
#9665=ADVANCED_FACE ( 'NONE', ( #7603 ), #1242, .T. ) ;
#9670=CARTESIAN_POINT ( 'NONE',  ( 0.000000000000000000, 316.7545334744432353, 495.1946179577816451 ) ) ;
#9681=CIRCLE ( 'NONE', #9033, 3.883636366625808911 ) ;
#9682=COLOUR_RGB ( '', 0.72549020, 0.75294118, 0.79215686) ;
#9698=CARTESIAN_POINT ( 'NONE',  ( -78.99999999999995737, 141.6406393683236331, 501.8237260975782874 ) ) ;
#9700=VECTOR ( 'NONE', #12707, 1000.000000000000000 ) ;
#9701=LINE ( 'NONE', #10006, #19873 ) ;
#9706=ORIENTED_EDGE ( 'NONE', *, *, #8989, .T. ) ;
#9715=CARTESIAN_POINT ( 'NONE',  ( -64.99999999999995737, 317.7545334744432353, 495.1946179577816451 ) ) ;
#9730=VECTOR ( 'NONE', #12622, 1000.000000000000000 ) ;
#9738=CARTESIAN_POINT ( 'NONE',  ( -41.50085094405407915, 175.4489062796178871, 510.3921618609452935 ) ) ;
#9741=CARTESIAN_POINT ( 'NONE',  ( 0.1778267103069386679, 139.8640615783817793, 489.1502978112980600 ) ) ;
#9743=ORIENTED_EDGE ( 'NONE', *, *, #12487, .T. ) ;
#9761=AXIS2_PLACEMENT_3D ( 'NONE', #14329, #12791, #392 ) ;
#9764=EDGE_CURVE ( 'NONE', #13515, #2973, #539, .T. ) ;
#9766=ORIENTED_EDGE ( 'NONE', *, *, #16475, .F. ) ;
#9772=( NAMED_UNIT ( * ) SI_UNIT ( $, .STERADIAN. ) SOLID_ANGLE_UNIT ( ) );
#9773=ORIENTED_EDGE ( 'NONE', *, *, #9948, .F. ) ;
#9786=EDGE_CURVE ( 'NONE', #6397, #2527, #3528, .T. ) ;
#9809=AXIS2_PLACEMENT_3D ( 'NONE', #329, #6326, #12604 ) ;
#9825=AXIS2_PLACEMENT_3D ( 'NONE', #3255, #1683, #358 ) ;
#9826=ORIENTED_EDGE ( 'NONE', *, *, #15420, .F. ) ;
#9828=DIRECTION ( 'NONE',  ( 1.000000000000000000, 0.000000000000000000, 0.000000000000000000 ) ) ;
#9831=DIRECTION ( 'NONE',  ( 0.000000000000000000, 0.000000000000000000, -1.000000000000000000 ) ) ;
#9836=CARTESIAN_POINT ( 'NONE',  ( -41.50085094405407915, 159.0821755739672483, 505.3921618609452935 ) ) ;
#9843=DIRECTION ( 'NONE',  ( 0.000000000000000000, -1.000000000000000000, -1.632680918566406793E-16 ) ) ;
#9844=CARTESIAN_POINT ( 'NONE',  ( -41.50085094405408626, 209.4098724938429541, 505.3921618609452935 ) ) ;
#9847=CARTESIAN_POINT ( 'NONE',  ( 1.181929469892510243, 139.7703989349544145, 490.5655098179848892 ) ) ;
#9857=EDGE_CURVE ( 'NONE', #2216, #469, #11608, .T. ) ;
#9869=DIRECTION ( 'NONE',  ( -0.000000000000000000, -0.000000000000000000, 1.000000000000000000 ) ) ;
#9872=CARTESIAN_POINT ( 'NONE',  ( -1.000000000000000888, 138.7545334744432637, 477.3411705753777596 ) ) ;
#9873=CARTESIAN_POINT ( 'NONE',  ( -58.16843972078500258, 319.7545334744432353, 485.1700099148404206 ) ) ;
#9877=LINE ( 'NONE', #9670, #19688 ) ;
#9881=ORIENTED_EDGE ( 'NONE', *, *, #17310, .F. ) ;
#9884=ORIENTED_EDGE ( 'NONE', *, *, #19355, .T. ) ;
#9886=ORIENTED_EDGE ( 'NONE', *, *, #10914, .T. ) ;
#9887=LINE ( 'NONE', #16199, #14356 ) ;
#9888=CARTESIAN_POINT ( 'NONE',  ( -82.18192946989243808, 216.7545334744432921, 490.5655098179832976 ) ) ;
#9898=( GEOMETRIC_REPRESENTATION_CONTEXT ( 3 ) GLOBAL_UNCERTAINTY_ASSIGNED_CONTEXT ( ( #14926 ) ) GLOBAL_UNIT_ASSIGNED_CONTEXT ( ( #17213, #3097, #9389 ) ) REPRESENTATION_CONTEXT ( 'NONE', 'WORKASPACE' ) );
#9907=VECTOR ( 'NONE', #3646, 1000.000000000000000 ) ;
#9911=ORIENTED_EDGE ( 'NONE', *, *, #12021, .T. ) ;
#9916=DIRECTION ( 'NONE',  ( 1.000000000000000000, 0.000000000000000000, 0.000000000000000000 ) ) ;
#9922=EDGE_CURVE ( 'NONE', #14767, #13515, #866, .T. ) ;
#9924=CIRCLE ( 'NONE', #13218, 1.000000000000015987 ) ;
#9939=AXIS2_PLACEMENT_3D ( 'NONE', #14188, #15552, #14091 ) ;
#9941=UNCERTAINTY_MEASURE_WITH_UNIT (LENGTH_MEASURE( 1.000000000000000082E-05 ), #353, 'distance_accuracy_value', 'NONE');
#9947=DIRECTION ( 'NONE',  ( -1.000000000000000000, 0.000000000000000000, 0.000000000000000000 ) ) ;
#9948=EDGE_CURVE ( 'NONE', #792, #9243, #10772, .T. ) ;
#9949=CARTESIAN_POINT ( 'NONE',  ( -38.50085094405407204, 175.4489062796178871, 505.3921618609452935 ) ) ;
#9964=EDGE_LOOP ( 'NONE', ( #20304, #3698, #959, #9061 ) ) ;
#9966=SURFACE_SIDE_STYLE ('',( #3683 ) ) ;
#9971=CARTESIAN_POINT ( 'NONE',  ( 0.09716098387576603546, 139.9221803985388419, 489.0003711267692665 ) ) ;
#9974=STYLED_ITEM ( 'NONE', ( #5124 ), #3479 ) ;
#9982=AXIS2_PLACEMENT_3D ( 'NONE', #19185, #10124, #8563 ) ;
#9985=EDGE_LOOP ( 'NONE', ( #16765, #4302, #4538, #8399 ) ) ;
#9991=FILL_AREA_STYLE_COLOUR ( '', #10741 ) ;
#10006=CARTESIAN_POINT ( 'NONE',  ( -44.50085094405407915, 175.4489062796178871, 510.3921618609452935 ) ) ;
#10012=ORIENTED_EDGE ( 'NONE', *, *, #11758, .F. ) ;
#10014=LINE ( 'NONE', #5278, #12343 ) ;
#10015=ORIENTED_EDGE ( 'NONE', *, *, #15614, .F. ) ;
#10024=CARTESIAN_POINT ( 'NONE',  ( -79.99999999999995737, 216.7545334744432921, 512.1946179577817020 ) ) ;
#10026=AXIS2_PLACEMENT_3D ( 'NONE', #6460, #17874, #11185 ) ;
#10033=EDGE_CURVE ( 'NONE', #3885, #12344, #15454, .T. ) ;
#10040=AXIS2_PLACEMENT_3D ( 'NONE', #8223, #11611, #14601 ) ;
#10046=CIRCLE ( 'NONE', #5770, 1.000000000000000000 ) ;
#10052=ORIENTED_EDGE ( 'NONE', *, *, #11529, .T. ) ;
#10057=DIRECTION ( 'NONE',  ( 0.000000000000000000, -0.7071067811865198172, -0.7071067811865753283 ) ) ;
#10060=( NAMED_UNIT ( * ) PLANE_ANGLE_UNIT ( ) SI_UNIT ( $, .RADIAN. ) );
#10067=ORIENTED_EDGE ( 'NONE', *, *, #14666, .F. ) ;
#10070=ORIENTED_EDGE ( 'NONE', *, *, #12184, .F. ) ;
#10073=VERTEX_POINT ( 'NONE', #12211 ) ;
#10076=VERTEX_POINT ( 'NONE', #18486 ) ;
#10082=CARTESIAN_POINT ( 'NONE',  ( -6.662140296159640225E-13, 139.7703989349544145, 490.5655098179848892 ) ) ;
#10096=ORIENTED_EDGE ( 'NONE', *, *, #6559, .F. ) ;
#10097=CARTESIAN_POINT ( 'NONE',  ( -78.99999999999995737, 139.2066006846527841, 488.2525619656395861 ) ) ;
#10115=ORIENTED_EDGE ( 'NONE', *, *, #7123, .T. ) ;
#10116=VERTEX_POINT ( 'NONE', #3461 ) ;
#10120=CARTESIAN_POINT ( 'NONE',  ( -64.99999999999995737, 317.7545334744432353, 475.1454018718993098 ) ) ;
#10122=CARTESIAN_POINT ( 'NONE',  ( 2.181929469892980755, 147.7545334744432921, 496.6642397995873921 ) ) ;
#10124=DIRECTION ( 'NONE',  ( -1.962615573354757393E-14, -0.7071067811865614505, 0.7071067811865336949 ) ) ;
#10127=CARTESIAN_POINT ( 'NONE',  ( -1.387778780781445676E-14, 138.7545334744432637, 500.8237260975782874 ) ) ;
#10135=AXIS2_PLACEMENT_3D ( 'NONE', #14503, #377, #3596 ) ;
#10144=DIRECTION ( 'NONE',  ( -0.000000000000000000, 0.000000000000000000, -1.000000000000000000 ) ) ;
#10151=PRESENTATION_STYLE_ASSIGNMENT (( #13160 ) ) ;
#10166=LINE ( 'NONE', #3795, #5281 ) ;
#10168=CARTESIAN_POINT ( 'NONE',  ( 0.1728887654703882282, 138.9434236829201836, 489.1421846862349412 ) ) ;
#10172=CARTESIAN_POINT ( 'NONE',  ( -79.99999999999995737, 152.4824555358011082, 477.3411705753777596 ) ) ;
#10179=CARTESIAN_POINT ( 'NONE',  ( -78.99999999999995737, 152.4824555358011082, 477.3411705753777596 ) ) ;
#10189=CARTESIAN_POINT ( 'NONE',  ( -58.16843972078500258, 317.7545334744432353, 481.2863735482146126 ) ) ;
#10195=CARTESIAN_POINT ( 'NONE',  ( -80.04214025239892294, 139.0005848764406551, 488.9285551588898215 ) ) ;
#10201=CARTESIAN_POINT ( 'NONE',  ( -79.99999999999995737, 138.7545334744432637, 509.3921618609452935 ) ) ;
#10212=ORIENTED_EDGE ( 'NONE', *, *, #11437, .T. ) ;
#10219=LINE ( 'NONE', #3940, #16818 ) ;
#10221=VERTEX_POINT ( 'NONE', #7167 ) ;
#10224=VECTOR ( 'NONE', #9828, 1000.000000000000000 ) ;
#10232=EDGE_CURVE ( 'NONE', #10073, #9264, #14875, .T. ) ;
#10243=DIRECTION ( 'NONE',  ( 0.000000000000000000, -1.632680918566406547E-16, 1.000000000000000000 ) ) ;
#10247=LINE ( 'NONE', #5917, #1632 ) ;
#10257=EDGE_LOOP ( 'NONE', ( #19642, #13846, #3789, #19582 ) ) ;
#10265=FILL_AREA_STYLE_COLOUR ( '', #5035 ) ;
#10269=CARTESIAN_POINT ( 'NONE',  ( -1.301042606982605321E-14, 140.0734055309426083, 488.6914064109051878 ) ) ;
#10274=FILL_AREA_STYLE_COLOUR ( '', #11264 ) ;
#10289=DIRECTION ( 'NONE',  ( -1.000000000000000000, -0.000000000000000000, -0.000000000000000000 ) ) ;
#10291=DIRECTION ( 'NONE',  ( 1.000000000000000000, -4.371814833150063998E-14, -1.016981637791458695E-13 ) ) ;
#10296=FILL_AREA_STYLE_COLOUR ( '', #18517 ) ;
#10308=VECTOR ( 'NONE', #8138, 1000.000000000000000 ) ;
#10313=ORIENTED_EDGE ( 'NONE', *, *, #15811, .F. ) ;
#10315=AXIS2_PLACEMENT_3D ( 'NONE', #12964, #17576, #4604 ) ;
#10316=ORIENTED_EDGE ( 'NONE', *, *, #17075, .F. ) ;
#10321=DIRECTION ( 'NONE',  ( 1.000000000000000000, 0.000000000000000000, 3.328238341717372086E-14 ) ) ;
#10322=CARTESIAN_POINT ( 'NONE',  ( -1.000000000000021094, 147.7545334744432921, 496.6642397995874489 ) ) ;
#10326=CARTESIAN_POINT ( 'NONE',  ( -81.00000000000127898, 139.7703989349544997, 489.5655098179835818 ) ) ;
#10328=VERTEX_POINT ( 'NONE', #12288 ) ;
#10330=CARTESIAN_POINT ( 'NONE',  ( 1.000000000001310063, 216.7545334744432921, 489.5655098179835818 ) ) ;
#10336=AXIS2_PLACEMENT_3D ( 'NONE', #12139, #5771, #891 ) ;
#10348=CARTESIAN_POINT ( 'NONE',  ( -80.84381259993401159, 139.4861549369088038, 500.2186618848270996 ) ) ;
#10351=CARTESIAN_POINT ( 'NONE',  ( -80.99999999999995737, 139.4861549369088323, 500.2186618848270996 ) ) ;
#10352=CARTESIAN_POINT ( 'NONE',  ( -81.18192946989275072, 139.4861549369088323, 500.2186618848270996 ) ) ;
#10376=FILL_AREA_STYLE ('',( #10265 ) ) ;
#10388=DIRECTION ( 'NONE',  ( 0.000000000000000000, 0.000000000000000000, -1.000000000000000000 ) ) ;
#10412=EDGE_CURVE ( 'NONE', #2362, #12373, #8176, .T. ) ;
#10425=ORIENTED_EDGE ( 'NONE', *, *, #7873, .T. ) ;
#10426=DIRECTION ( 'NONE',  ( 1.000000000000000000, 0.000000000000000000, 0.000000000000000000 ) ) ;
#10433=SURFACE_STYLE_USAGE ( .BOTH. , #1010 ) ;
#10435=CARTESIAN_POINT ( 'NONE',  ( -80.51861556725816627, 138.8636137914787696, 489.4457938216992261 ) ) ;
#10442=ORIENTED_EDGE ( 'NONE', *, *, #3852, .T. ) ;
#10443=ORIENTED_EDGE ( 'NONE', *, *, #4440, .F. ) ;
#10452=STYLED_ITEM ( 'NONE', ( #6080 ), #3975 ) ;
#10455=DIRECTION ( 'NONE',  ( -1.000000000000000000, 0.000000000000000000, 0.000000000000000000 ) ) ;
#10475=CARTESIAN_POINT ( 'NONE',  ( 1.181929469854658965, 139.7545334744432637, -9.119545354731954390E-14 ) ) ;
#10489=DIRECTION ( 'NONE',  ( -0.000000000000000000, -1.000000000000000000, -0.000000000000000000 ) ) ;
#10496=FACE_OUTER_BOUND ( 'NONE', #11534, .T. ) ;
#10517=ADVANCED_FACE ( 'NONE', ( #16334 ), #6742, .F. ) ;
#10523=EDGE_CURVE ( 'NONE', #8826, #8340, #2168, .T. ) ;
#10531=FACE_OUTER_BOUND ( 'NONE', #2621, .T. ) ;
#10539=UNCERTAINTY_MEASURE_WITH_UNIT (LENGTH_MEASURE( 1.000000000000000082E-05 ), #2320, 'distance_accuracy_value', 'NONE');
#10545=DIRECTION ( 'NONE',  ( 1.000000000000000000, 0.000000000000000000, 0.000000000000000000 ) ) ;
#10549=AXIS2_PLACEMENT_3D ( 'NONE', #4324, #2563, #4426 ) ;
#10551=CARTESIAN_POINT ( 'NONE',  ( -80.06977618402036967, 141.0668072968081503, 501.4424506789935094 ) ) ;
#10555=ORIENTED_EDGE ( 'NONE', *, *, #13493, .F. ) ;
#10571=DIRECTION ( 'NONE',  ( -7.715811803773179210E-14, 0.000000000000000000, -1.000000000000000000 ) ) ;
#10578=CARTESIAN_POINT ( 'NONE',  ( 0.000000000000000000, 316.7545334744432921, 205.1946179577815883 ) ) ;
#10584=AXIS2_PLACEMENT_3D ( 'NONE', #15444, #3268, #7709 ) ;
#10588=DIRECTION ( 'NONE',  ( 0.000000000000000000, 1.000000000000000000, -0.000000000000000000 ) ) ;
#10593=ORIENTED_EDGE ( 'NONE', *, *, #14538, .F. ) ;
#10612=FACE_BOUND ( 'NONE', #248, .T. ) ;
#10616=DIRECTION ( 'NONE',  ( 0.000000000000000000, 0.000000000000000000, -1.000000000000000000 ) ) ;
#10624=DIRECTION ( 'NONE',  ( -0.000000000000000000, -1.000000000000000000, -0.000000000000000000 ) ) ;
#10626=DIRECTION ( 'NONE',  ( 0.000000000000000000, 0.000000000000000000, -1.000000000000000000 ) ) ;
#10627=CARTESIAN_POINT ( 'NONE',  ( -79.66506982498428613, 138.8257004745550773, 489.9345105970523946 ) ) ;
#10628=COLOUR_RGB ( '', 0.72549020, 0.75294118, 0.79215686) ;
#10647=VECTOR ( 'NONE', #12644, 1000.000000000000000 ) ;
#10649=SURFACE_SIDE_STYLE ('',( #18369 ) ) ;
#10655=EDGE_CURVE ( 'NONE', #12344, #10821, #3469, .T. ) ;
#10661=ADVANCED_FACE ( 'NONE', ( #6184 ), #13657, .T. ) ;
#10664=VECTOR ( 'NONE', #1680, 1000.000000000000000 ) ;
#10665=( GEOMETRIC_REPRESENTATION_CONTEXT ( 3 ) GLOBAL_UNCERTAINTY_ASSIGNED_CONTEXT ( ( #18342 ) ) GLOBAL_UNIT_ASSIGNED_CONTEXT ( ( #18048, #11376, #8395 ) ) REPRESENTATION_CONTEXT ( 'NONE', 'WORKASPACE' ) );
#10669=CARTESIAN_POINT ( 'NONE',  ( 0.2320613958866641346, 140.7529646695461736, 501.1799789315547287 ) ) ;
#10673=CARTESIAN_POINT ( 'NONE',  ( -41.50085094405407915, 175.4489062796178871, 505.3921618609452935 ) ) ;
#10701=ORIENTED_EDGE ( 'NONE', *, *, #12318, .T. ) ;
#10703=AXIS2_PLACEMENT_3D ( 'NONE', #9844, #8306, #14579 ) ;
#10709=DIRECTION ( 'NONE',  ( 0.000000000000000000, -0.6449357872488920007, -0.7642367632649269549 ) ) ;
#10714=DIRECTION ( 'NONE',  ( 0.000000000000000000, 0.000000000000000000, -1.000000000000000000 ) ) ;
#10719=EDGE_LOOP ( 'NONE', ( #1789, #20048, #9881 ) ) ;
#10720=EDGE_LOOP ( 'NONE', ( #1564, #16242, #11586, #8432 ) ) ;
#10724=VERTEX_POINT ( 'NONE', #15456 ) ;
#10729=DIRECTION ( 'NONE',  ( 0.000000000000000000, -0.7071067811865336949, 0.7071067811865614505 ) ) ;
#10737=CARTESIAN_POINT ( 'NONE',  ( -0.4453075966856865908, 139.8159989653383661, 500.9064470951030330 ) ) ;
#10739=LINE ( 'NONE', #12394, #18562 ) ;
#10741=COLOUR_RGB ( '', 0.31764706, 0.68627451, 0.89019608) ;
#10752=CARTESIAN_POINT ( 'NONE',  ( -78.99999999999995737, 139.2066006846527841, 488.2525619656395861 ) ) ;
#10765=FACE_OUTER_BOUND ( 'NONE', #8937, .T. ) ;
#10766=ORIENTED_EDGE ( 'NONE', *, *, #10924, .F. ) ;
#10772=LINE ( 'NONE', #17061, #218 ) ;
#10775=CARTESIAN_POINT ( 'NONE',  ( -1.242741617435013737E-14, 216.7545334744432921, 501.8237260975781737 ) ) ;
#10780=DIRECTION ( 'NONE',  ( -0.000000000000000000, -0.000000000000000000, 1.000000000000000000 ) ) ;
#10804=ADVANCED_FACE ( 'NONE', ( #14916 ), #3398, .T. ) ;
#10812=DIRECTION ( 'NONE',  ( 1.450371633464475582E-15, 0.000000000000000000, 1.000000000000000000 ) ) ;
#10818=( NAMED_UNIT ( * ) SI_UNIT ( $, .STERADIAN. ) SOLID_ANGLE_UNIT ( ) );
#10821=VERTEX_POINT ( 'NONE', #14808 ) ;
#10825=SURFACE_STYLE_FILL_AREA ( #1619 ) ;
#10835=ORIENTED_EDGE ( 'NONE', *, *, #5848, .T. ) ;
#10837=DIRECTION ( 'NONE',  ( 7.715811803773179210E-14, -0.000000000000000000, 1.000000000000000000 ) ) ;
#10840=VERTEX_POINT ( 'NONE', #7195 ) ;
#10851=CARTESIAN_POINT ( 'NONE',  ( -0.06844068954109454317, 140.2957399442693429, 501.7113191689081191 ) ) ;
#10854=ADVANCED_FACE ( 'NONE', ( #7293 ), #4501, .F. ) ;
#10872=CARTESIAN_POINT ( 'NONE',  ( -2.959702524295976245E-14, 141.4901731731944210, 501.7345762936599272 ) ) ;
#10875=DIRECTION ( 'NONE',  ( -1.135258727068398879E-15, 0.000000000000000000, 1.000000000000000000 ) ) ;
#10884=VERTEX_POINT ( 'NONE', #13868 ) ;
#10890=DIRECTION ( 'NONE',  ( -1.025567617263343161E-15, -0.7071067811865455743, -0.7071067811865493491 ) ) ;
#10894=AXIS2_PLACEMENT_3D ( 'NONE', #438, #3331, #14558 ) ;
#10908=ORIENTED_EDGE ( 'NONE', *, *, #8167, .F. ) ;
#10910=TOROIDAL_SURFACE ( 'NONE', #2329, 8.000000000000000000, 1.000000000000000000 ) ;
#10914=EDGE_CURVE ( 'NONE', #5827, #18716, #9519, .T. ) ;
#10917=CARTESIAN_POINT ( 'NONE',  ( -81.18192946989245229, 138.7545334744432637, 491.0690926367356610 ) ) ;
#10919=DIRECTION ( 'NONE',  ( 0.000000000000000000, 0.000000000000000000, -1.000000000000000000 ) ) ;
#10924=EDGE_CURVE ( 'NONE', #17380, #19179, #11170, .T. ) ;
#10928=ORIENTED_EDGE ( 'NONE', *, *, #17469, .F. ) ;
#10929=SURFACE_STYLE_FILL_AREA ( #3194 ) ;
#10930=VECTOR ( 'NONE', #6576, 1000.000000000000000 ) ;
#10936=DIRECTION ( 'NONE',  ( -0.000000000000000000, -1.000000000000000000, -0.000000000000000000 ) ) ;
#10943=CARTESIAN_POINT ( 'NONE',  ( 0.6927201199992654157, 139.4947537936898243, 500.2388491393129470 ) ) ;
#10957=AXIS2_PLACEMENT_3D ( 'NONE', #918, #19776, #19887 ) ;
#10963=FACE_OUTER_BOUND ( 'NONE', #11814, .T. ) ;
#10968=ORIENTED_EDGE ( 'NONE', *, *, #9786, .T. ) ;
#10973=ORIENTED_EDGE ( 'NONE', *, *, #6801, .F. ) ;
#10978=ORIENTED_EDGE ( 'NONE', *, *, #2740, .T. ) ;
#11005=CARTESIAN_POINT ( 'NONE',  ( -80.02377347867404467, 140.1169800153989513, 501.4439172727915661 ) ) ;
#11008=EDGE_CURVE ( 'NONE', #17234, #14850, #14580, .T. ) ;
#11019=EDGE_CURVE ( 'NONE', #11867, #14850, #5418, .T. ) ;
#11025=EDGE_CURVE ( 'NONE', #2815, #20158, #12489, .T. ) ;
#11030=ORIENTED_EDGE ( 'NONE', *, *, #1925, .F. ) ;
#11031=UNCERTAINTY_MEASURE_WITH_UNIT (LENGTH_MEASURE( 1.000000000000000082E-05 ), #4271, 'distance_accuracy_value', 'NONE');
#11034=DIRECTION ( 'NONE',  ( 0.000000000000000000, -0.000000000000000000, -1.000000000000000000 ) ) ;
#11039=DIRECTION ( 'NONE',  ( 0.000000000000000000, -0.7071067811865336949, -0.7071067811865614505 ) ) ;
#11045=CARTESIAN_POINT ( 'NONE',  ( -81.18192946989263703, 147.7545334744432921, 496.6642397995874489 ) ) ;
#11047=LINE ( 'NONE', #14037, #16257 ) ;
#11058=ADVANCED_FACE ( 'NONE', ( #11490 ), #19316, .T. ) ;
#11065=CARTESIAN_POINT ( 'NONE',  ( 0.4596639520886662278, 140.5461004730986474, 500.9794230863846565 ) ) ;
#11075=VERTEX_POINT ( 'NONE', #10352 ) ;
#11077=( GEOMETRIC_REPRESENTATION_CONTEXT ( 3 ) GLOBAL_UNCERTAINTY_ASSIGNED_CONTEXT ( ( #3868 ) ) GLOBAL_UNIT_ASSIGNED_CONTEXT ( ( #2343, #16490, #18215 ) ) REPRESENTATION_CONTEXT ( 'NONE', 'WORKASPACE' ) );
#11088=EDGE_CURVE ( 'NONE', #9264, #3611, #20366, .T. ) ;
#11091=LINE ( 'NONE', #162, #16509 ) ;
#11102=CARTESIAN_POINT ( 'NONE',  ( -80.38765499834516959, 139.8541360342012183, 501.0141826477431550 ) ) ;
#11116=ADVANCED_FACE ( 'NONE', ( #5825 ), #4476, .F. ) ;
#11150=ORIENTED_EDGE ( 'NONE', *, *, #3753, .T. ) ;
#11154=CARTESIAN_POINT ( 'NONE',  ( -0.9641265287173192977, 140.4732238075575026, 501.9632754140384918 ) ) ;
#11156=CARTESIAN_POINT ( 'NONE',  ( -80.99999999999995737, 216.7545334744432921, 488.5655098179835818 ) ) ;
#11164=CARTESIAN_POINT ( 'NONE',  ( -79.99999999999995737, 216.7545334744432921, 155.1946179577816167 ) ) ;
#11170=CIRCLE ( 'NONE', #6571, 1.000000000000000888 ) ;
#11181=AXIS2_PLACEMENT_3D ( 'NONE', #19966, #19655, #10714 ) ;
#11185=DIRECTION ( 'NONE',  ( 7.719519468096785259E-14, 0.000000000000000000, 1.000000000000000000 ) ) ;
#11196=ADVANCED_FACE ( 'NONE', ( #11255 ), #3326, .T. ) ;
#11197=VECTOR ( 'NONE', #17645, 1000.000000000000000 ) ;
#11200=CARTESIAN_POINT ( 'NONE',  ( -81.00000000000065370, 140.4048636633015406, 500.8237260975782874 ) ) ;
#11210=CARTESIAN_POINT ( 'NONE',  ( -1.000000000000001110, 152.4824555358011082, 478.3411705753777596 ) ) ;
#11213=CARTESIAN_POINT ( 'NONE',  ( -44.50085094405407915, 175.4489062796178871, 510.3921618609452935 ) ) ;
#11224=( NAMED_UNIT ( * ) PLANE_ANGLE_UNIT ( ) SI_UNIT ( $, .RADIAN. ) );
#11226=CARTESIAN_POINT ( 'NONE',  ( -1.170604780609796557E-14, 142.0976792249508946, 502.3210940490797611 ) ) ;
#11235=LINE ( 'NONE', #108, #18236 ) ;
#11237=DIRECTION ( 'NONE',  ( 0.000000000000000000, -1.000000000000000000, 0.000000000000000000 ) ) ;
#11242=ADVANCED_FACE ( 'NONE', ( #12724 ), #15812, .F. ) ;
#11245=CARTESIAN_POINT ( 'NONE',  ( -79.99999999999995737, 216.7545334744432921, 495.1946179577816451 ) ) ;
#11253=CARTESIAN_POINT ( 'NONE',  ( -0.3034418303818310347, 139.7372778959907578, 500.7550088380377247 ) ) ;
#11255=FACE_OUTER_BOUND ( 'NONE', #18378, .T. ) ;
#11257=CARTESIAN_POINT ( 'NONE',  ( -79.04867202909733237, 139.0343723396696873, 488.8251854762526136 ) ) ;
#11262=EDGE_CURVE ( 'NONE', #2973, #10724, #12444, .T. ) ;
#11263=ORIENTED_EDGE ( 'NONE', *, *, #3599, .T. ) ;
#11264=COLOUR_RGB ( '', 0.72549020, 0.75294118, 0.79215686) ;
#11279=CARTESIAN_POINT ( 'NONE',  ( -80.47490325750347040, 139.7918628025659586, 489.4274594641468639 ) ) ;
#11300=ORIENTED_EDGE ( 'NONE', *, *, #667, .T. ) ;
#11305=CARTESIAN_POINT ( 'NONE',  ( -79.99999999999995737, 216.7545334744432921, 155.1946179577816167 ) ) ;
#11308=CARTESIAN_POINT ( 'NONE',  ( -1.242741617435013737E-14, 141.6406393683235194, 501.8237260975781737 ) ) ;
#11311=VECTOR ( 'NONE', #8022, 1000.000000000000000 ) ;
#11318=CARTESIAN_POINT ( 'NONE',  ( -1.000000000000014655, 152.4824555358010798, 501.3921618609452366 ) ) ;
#11330=CARTESIAN_POINT ( 'NONE',  ( 0.9999999999998859801, 216.7545334744432921, 500.8237260975781737 ) ) ;
#11337=FACE_OUTER_BOUND ( 'NONE', #15101, .T. ) ;
#11344=LINE ( 'NONE', #1433, #3113 ) ;
#11351=AXIS2_PLACEMENT_3D ( 'NONE', #15153, #12076, #20020 ) ;
#11353=ORIENTED_EDGE ( 'NONE', *, *, #13535, .F. ) ;
#11356=ORIENTED_EDGE ( 'NONE', *, *, #6217, .F. ) ;
#11371=CARTESIAN_POINT ( 'NONE',  ( -79.96164301880533287, 139.1521635470821536, 488.4177740748586984 ) ) ;
#11376=( NAMED_UNIT ( * ) PLANE_ANGLE_UNIT ( ) SI_UNIT ( $, .RADIAN. ) );
#11385=AXIS2_PLACEMENT_3D ( 'NONE', #10122, #13335, #11776 ) ;
#11390=DIRECTION ( 'NONE',  ( 1.000000000000000000, 0.000000000000000000, 0.000000000000000000 ) ) ;
#11392=LINE ( 'NONE', #12843, #7994 ) ;
#11394=( NAMED_UNIT ( * ) PLANE_ANGLE_UNIT ( ) SI_UNIT ( $, .RADIAN. ) );
#11397=PLANE ( 'NONE',  #2762 ) ;
#11399=DIRECTION ( 'NONE',  ( -1.000000000000000000, -0.000000000000000000, -0.000000000000000000 ) ) ;
#11404=ADVANCED_FACE ( 'NONE', ( #8387 ), #17654, .F. ) ;
#11406=DIRECTION ( 'NONE',  ( 0.000000000000000000, -1.000000000000000000, 0.000000000000000000 ) ) ;
#11407=DIRECTION ( 'NONE',  ( -1.000000000000000000, 0.000000000000000000, 1.322948291343117631E-12 ) ) ;
#11414=CARTESIAN_POINT ( 'NONE',  ( -1.387778780781445676E-14, 216.7545334744432921, 489.5655098179848892 ) ) ;
#11433=ORIENTED_EDGE ( 'NONE', *, *, #16475, .T. ) ;
#11437=EDGE_CURVE ( 'NONE', #19090, #7676, #3744, .T. ) ;
#11447=CYLINDRICAL_SURFACE ( 'NONE', #565, 1.000000000000000888 ) ;
#11462=ORIENTED_EDGE ( 'NONE', *, *, #6169, .F. ) ;
#11463=CARTESIAN_POINT ( 'NONE',  ( -41.50085094405408626, 193.0431417881923153, 505.3921618609452935 ) ) ;
#11469=DIRECTION ( 'NONE',  ( -1.000000000000000000, -0.000000000000000000, 0.000000000000000000 ) ) ;
#11471=VERTEX_POINT ( 'NONE', #1121 ) ;
#11474=CARTESIAN_POINT ( 'NONE',  ( -81.18192946989242387, 139.7703989349477354, 489.5655098179833544 ) ) ;
#11475=DIRECTION ( 'NONE',  ( 3.392348130799086764E-14, 0.000000000000000000, -1.000000000000000000 ) ) ;
#11482=DIRECTION ( 'NONE',  ( 0.000000000000000000, 1.000000000000000000, 0.000000000000000000 ) ) ;
#11486=EDGE_CURVE ( 'NONE', #17127, #5083, #2794, .T. ) ;
#11488=SURFACE_STYLE_USAGE ( .BOTH. , #19221 ) ;
#11490=FACE_OUTER_BOUND ( 'NONE', #8533, .T. ) ;
#11499=AXIS2_PLACEMENT_3D ( 'NONE', #7268, #8809, #20116 ) ;
#11501=EDGE_CURVE ( 'NONE', #15750, #19125, #6017, .T. ) ;
#11503=ORIENTED_EDGE ( 'NONE', *, *, #16964, .T. ) ;
#11511=EDGE_CURVE ( 'NONE', #19976, #17153, #12087, .T. ) ;
#11512=CIRCLE ( 'NONE', #14132, 3.000000000000009770 ) ;
#11517=CARTESIAN_POINT ( 'NONE',  ( -0.9517357342956975774, 139.0345459197187097, 488.8243121191512159 ) ) ;
#11518=LINE ( 'NONE', #9872, #1414 ) ;
#11520=CARTESIAN_POINT ( 'NONE',  ( -1.000000000000000888, 138.7545334744432637, 509.3921618609452935 ) ) ;
#11525=ORIENTED_EDGE ( 'NONE', *, *, #4793, .T. ) ;
#11529=EDGE_CURVE ( 'NONE', #1021, #13854, #13822, .T. ) ;
#11533=EDGE_LOOP ( 'NONE', ( #13109, #18897, #13717, #16127 ) ) ;
#11534=EDGE_LOOP ( 'NONE', ( #13787, #9911, #12810, #10212, #5529, #18785 ) ) ;
#11535=EDGE_LOOP ( 'NONE', ( #10968, #8303, #5954, #11030 ) ) ;
#11541=DIRECTION ( 'NONE',  ( 0.000000000000000000, -1.000000000000000000, 0.000000000000000000 ) ) ;
#11543=AXIS2_PLACEMENT_3D ( 'NONE', #15919, #17434, #6327 ) ;
#11551=CARTESIAN_POINT ( 'NONE',  ( 0.000000000000000000, 216.7545334744432921, 510.3921618609452935 ) ) ;
#11562=CARTESIAN_POINT ( 'NONE',  ( -81.00000000000127898, 138.8810201506716169, 489.5655098179835818 ) ) ;
#11573=ORIENTED_EDGE ( 'NONE', *, *, #15811, .T. ) ;
#11577=ORIENTED_EDGE ( 'NONE', *, *, #3052, .T. ) ;
#11578=ORIENTED_EDGE ( 'NONE', *, *, #15897, .T. ) ;
#11579=AXIS2_PLACEMENT_3D ( 'NONE', #1490, #8004, #14283 ) ;
#11581=CIRCLE ( 'NONE', #9939, 8.000000000000007105 ) ;
#11582=ORIENTED_EDGE ( 'NONE', *, *, #1812, .T. ) ;
#11586=ORIENTED_EDGE ( 'NONE', *, *, #11486, .T. ) ;
#11591=FACE_OUTER_BOUND ( 'NONE', #19204, .T. ) ;
#11594=( LENGTH_UNIT ( ) NAMED_UNIT ( * ) SI_UNIT ( .MILLI., .METRE. ) );
#11603=VECTOR ( 'NONE', #1253, 1000.000000000000000 ) ;
#11608=LINE ( 'NONE', #5438, #15040 ) ;
#11611=DIRECTION ( 'NONE',  ( -1.000000000000000000, 0.000000000000000000, 0.000000000000000000 ) ) ;
#11612=ORIENTED_EDGE ( 'NONE', *, *, #9764, .T. ) ;
#11617=DIRECTION ( 'NONE',  ( 0.000000000000000000, 1.000000000000000000, 0.000000000000000000 ) ) ;
#11630=EDGE_CURVE ( 'NONE', #1465, #10073, #14226, .T. ) ;
#11632=ORIENTED_EDGE ( 'NONE', *, *, #12147, .F. ) ;
#11639=CYLINDRICAL_SURFACE ( 'NONE', #13614, 1.000000000000000888 ) ;
#11654=DIRECTION ( 'NONE',  ( 0.000000000000000000, 1.000000000000000000, 0.000000000000000000 ) ) ;
#11656=ORIENTED_EDGE ( 'NONE', *, *, #6117, .T. ) ;
#11657=AXIS2_PLACEMENT_3D ( 'NONE', #12960, #257, #17775 ) ;
#11667=LINE ( 'NONE', #3841, #12181 ) ;
#11677=DIRECTION ( 'NONE',  ( -1.017652531801993019E-13, 0.000000000000000000, -1.000000000000000000 ) ) ;
#11682=CARTESIAN_POINT ( 'NONE',  ( -79.99999999999995737, 152.4824555358010798, 509.3921618609452935 ) ) ;
#11684=CARTESIAN_POINT ( 'NONE',  ( -79.99999999999995737, 216.7545334744432921, 495.1946179577816451 ) ) ;
#11692=ORIENTED_EDGE ( 'NONE', *, *, #3052, .F. ) ;
#11693=( GEOMETRIC_REPRESENTATION_CONTEXT ( 3 ) GLOBAL_UNCERTAINTY_ASSIGNED_CONTEXT ( ( #19576 ) ) GLOBAL_UNIT_ASSIGNED_CONTEXT ( ( #3802, #6695, #6904 ) ) REPRESENTATION_CONTEXT ( 'NONE', 'WORKASPACE' ) );
#11710=ORIENTED_EDGE ( 'NONE', *, *, #16821, .T. ) ;
#11713=FILL_AREA_STYLE ('',( #3256 ) ) ;
#11717=VERTEX_POINT ( 'NONE', #6831 ) ;
#11719=ORIENTED_EDGE ( 'NONE', *, *, #9494, .T. ) ;
#11722=ORIENTED_EDGE ( 'NONE', *, *, #9948, .T. ) ;
#11728=DIRECTION ( 'NONE',  ( 0.000000000000000000, 0.000000000000000000, -1.000000000000000000 ) ) ;
#11743=ORIENTED_EDGE ( 'NONE', *, *, #10914, .F. ) ;
#11745=EDGE_CURVE ( 'NONE', #6868, #5490, #8546, .T. ) ;
#11749=CYLINDRICAL_SURFACE ( 'NONE', #3514, 3.883636366625808911 ) ;
#11758=EDGE_CURVE ( 'NONE', #625, #5827, #6929, .T. ) ;
#11776=DIRECTION ( 'NONE',  ( 7.714098457234357737E-14, 6.938893903907222067E-15, 1.000000000000000000 ) ) ;
#11787=DIRECTION ( 'NONE',  ( 1.318389841742372180E-12, 0.000000000000000000, -1.000000000000000000 ) ) ;
#11801=CARTESIAN_POINT ( 'NONE',  ( 0.000000000000000000, 216.7545334744432921, 495.1946179577816451 ) ) ;
#11809=DIRECTION ( 'NONE',  ( -8.027491443112700323E-16, -0.7071067811865504593, 0.7071067811865445751 ) ) ;
#11814=EDGE_LOOP ( 'NONE', ( #5230, #3786, #11433, #13146 ) ) ;
#11818=EDGE_CURVE ( 'NONE', #18338, #16622, #979, .T. ) ;
#11820=VERTEX_POINT ( 'NONE', #16504 ) ;
#11828=CIRCLE ( 'NONE', #13480, 1.000000000000015987 ) ;
#11835=DIRECTION ( 'NONE',  ( -1.000000000000000000, 0.000000000000000000, -0.000000000000000000 ) ) ;
#11837=CARTESIAN_POINT ( 'NONE',  ( -78.99999999999995737, 152.4824555358010798, 509.3921618609452935 ) ) ;
#11850=DIRECTION ( 'NONE',  ( 0.000000000000000000, 0.000000000000000000, -1.000000000000000000 ) ) ;
#11852=DIRECTION ( 'NONE',  ( -0.000000000000000000, -1.000000000000000000, -0.000000000000000000 ) ) ;
#11867=VERTEX_POINT ( 'NONE', #5562 ) ;
#11875=FACE_OUTER_BOUND ( 'NONE', #16296, .T. ) ;
#11880=CYLINDRICAL_SURFACE ( 'NONE', #12703, 9.000000000000007105 ) ;
#11886=DIRECTION ( 'NONE',  ( -0.000000000000000000, 1.000000000000000000, -0.000000000000000000 ) ) ;
#11891=EDGE_CURVE ( 'NONE', #14767, #20158, #20065, .T. ) ;
#11904=CARTESIAN_POINT ( 'NONE',  ( -80.26761590469169505, 140.6967024680590441, 501.1310021303755207 ) ) ;
#11909=DIRECTION ( 'NONE',  ( 1.000000000000000000, 0.000000000000000000, 0.000000000000000000 ) ) ;
#11913=FACE_OUTER_BOUND ( 'NONE', #7529, .T. ) ;
#11918=EDGE_LOOP ( 'NONE', ( #14249, #362, #474, #599 ) ) ;
#11920=ORIENTED_EDGE ( 'NONE', *, *, #1537, .F. ) ;
#11926=AXIS2_PLACEMENT_3D ( 'NONE', #1046, #18478, #2824 ) ;
#11930=FACE_OUTER_BOUND ( 'NONE', #1905, .T. ) ;
#11932=FILL_AREA_STYLE ('',( #10274 ) ) ;
#11955=FACE_OUTER_BOUND ( 'NONE', #5626, .T. ) ;
#11972=CARTESIAN_POINT ( 'NONE',  ( -80.99999999999995737, 140.4048636633015406, 499.8237260975782874 ) ) ;
#11984=DIRECTION ( 'NONE',  ( -0.000000000000000000, -1.000000000000000000, -0.000000000000000000 ) ) ;
#12002=ORIENTED_EDGE ( 'NONE', *, *, #19579, .T. ) ;
#12009=AXIS2_PLACEMENT_3D ( 'NONE', #17017, #9079, #11034 ) ;
#12011=DIRECTION ( 'NONE',  ( 0.000000000000000000, 0.000000000000000000, -1.000000000000000000 ) ) ;
#12021=EDGE_CURVE ( 'NONE', #469, #17405, #14584, .T. ) ;
#12033=EDGE_CURVE ( 'NONE', #5083, #8090, #11091, .T. ) ;
#12040=ADVANCED_FACE ( 'NONE', ( #14277 ), #17372, .F. ) ;
#12042=LINE ( 'NONE', #5849, #14746 ) ;
#12043=LINE ( 'NONE', #13484, #2372 ) ;
#12048=AXIS2_PLACEMENT_3D ( 'NONE', #325, #6634, #12922 ) ;
#12052=DIRECTION ( 'NONE',  ( 0.000000000000000000, -1.000000000000000000, 0.000000000000000000 ) ) ;
#12061=CARTESIAN_POINT ( 'NONE',  ( -80.71807173247304945, 138.7734074251775667, 490.4856072914361107 ) ) ;
#12076=DIRECTION ( 'NONE',  ( 0.000000000000000000, 1.000000000000000000, 0.000000000000000000 ) ) ;
#12086=PLANE ( 'NONE',  #505 ) ;
#12087=LINE ( 'NONE', #18349, #5363 ) ;
#12088=CARTESIAN_POINT ( 'NONE',  ( -80.27485217873301337, 138.9115877469687348, 489.2627155145635243 ) ) ;
#12102=DIRECTION ( 'NONE',  ( 0.000000000000000000, 0.000000000000000000, 1.000000000000000000 ) ) ;
#12108=ORIENTED_EDGE ( 'NONE', *, *, #6729, .T. ) ;
#12113=DIRECTION ( 'NONE',  ( 1.000000000000000000, 0.000000000000000000, 0.000000000000000000 ) ) ;
#12123=CYLINDRICAL_SURFACE ( 'NONE', #15758, 1.000000000000000000 ) ;
#12128=SURFACE_SIDE_STYLE ('',( #19941 ) ) ;
#12139=CARTESIAN_POINT ( 'NONE',  ( -1.000000000000014655, 152.4824555358011082, 486.3411705753778165 ) ) ;
#12143=COLOUR_RGB ( '', 0.09019608, 0.27058824, 0.51372549) ;
#12147=EDGE_CURVE ( 'NONE', #18810, #17220, #20371, .T. ) ;
#12162=ORIENTED_EDGE ( 'NONE', *, *, #8431, .F. ) ;
#12173=DIRECTION ( 'NONE',  ( 1.000000000000000000, 0.000000000000000000, 0.000000000000000000 ) ) ;
#12174=CARTESIAN_POINT ( 'NONE',  ( -81.18192946989242387, 139.7703989349477354, 490.5655098180907885 ) ) ;
#12181=VECTOR ( 'NONE', #9916, 1000.000000000000000 ) ;
#12184=EDGE_CURVE ( 'NONE', #584, #792, #3182, .T. ) ;
#12190=CARTESIAN_POINT ( 'NONE',  ( -80.99999999999995737, 140.4048636633015406, 500.8237260975782874 ) ) ;
#12201=VERTEX_POINT ( 'NONE', #14308 ) ;
#12208=LINE ( 'NONE', #5837, #15001 ) ;
#12211=CARTESIAN_POINT ( 'NONE',  ( -1.000000000000000888, 152.4824555358010798, 510.3921618609452935 ) ) ;
#12214=CARTESIAN_POINT ( 'NONE',  ( -44.50085094405410757, 209.4098724938429541, 505.3921618609452935 ) ) ;
#12217=FILL_AREA_STYLE ('',( #2433 ) ) ;
#12230=ORIENTED_EDGE ( 'NONE', *, *, #9116, .F. ) ;
#12232=ADVANCED_FACE ( 'NONE', ( #14502 ), #5339, .T. ) ;
#12244=( NAMED_UNIT ( * ) PLANE_ANGLE_UNIT ( ) SI_UNIT ( $, .RADIAN. ) );
#12249=DIRECTION ( 'NONE',  ( -1.000000000000000000, -0.000000000000000000, -0.000000000000000000 ) ) ;
#12250=EDGE_CURVE ( 'NONE', #8486, #6469, #16388, .T. ) ;
#12253=( GEOMETRIC_REPRESENTATION_CONTEXT ( 3 ) GLOBAL_UNCERTAINTY_ASSIGNED_CONTEXT ( ( #12381 ) ) GLOBAL_UNIT_ASSIGNED_CONTEXT ( ( #7295, #15122, #14921 ) ) REPRESENTATION_CONTEXT ( 'NONE', 'WORKASPACE' ) );
#12255=EDGE_CURVE ( 'NONE', #10724, #566, #2131, .T. ) ;
#12269=AXIS2_PLACEMENT_3D ( 'NONE', #7399, #12334, #20036 ) ;
#12274=DIRECTION ( 'NONE',  ( -1.000000000000000000, 0.000000000000000000, 0.000000000000000000 ) ) ;
#12275=CARTESIAN_POINT ( 'NONE',  ( 0.8442384278957183463, 139.4861549369088038, 500.2186618848268722 ) ) ;
#12276=ADVANCED_FACE ( 'NONE', ( #12983 ), #13186, .T. ) ;
#12277=CLOSED_SHELL ( 'NONE', ( #18329, #418, #11116, #12040, #6305, #3492, #1705, #18050, #12428, #3479, #9595, #2057 ) ) ;
#12283=ORIENTED_EDGE ( 'NONE', *, *, #6729, .F. ) ;
#12288=CARTESIAN_POINT ( 'NONE',  ( -1.450371633464476962E-15, 152.4824555358010798, 509.3921618609452935 ) ) ;
#12293=AXIS2_PLACEMENT_3D ( 'NONE', #2013, #9661, #6901 ) ;
#12295=CARTESIAN_POINT ( 'NONE',  ( -79.99999999999995737, 141.6406393683236331, 501.8237260975782874 ) ) ;
#12304=CARTESIAN_POINT ( 'NONE',  ( -58.16843972078500258, 319.7545334744432353, 481.2863735482146126 ) ) ;
#12306=ORIENTED_EDGE ( 'NONE', *, *, #9116, .T. ) ;
#12309=ORIENTED_EDGE ( 'NONE', *, *, #3852, .F. ) ;
#12315=CIRCLE ( 'NONE', #126, 1.000000000000000888 ) ;
#12318=EDGE_CURVE ( 'NONE', #1517, #1728, #11518, .T. ) ;
#12321=AXIS2_PLACEMENT_3D ( 'NONE', #8971, #15068, #8787 ) ;
#12324=DIRECTION ( 'NONE',  ( 1.000000000000000000, 0.000000000000000000, 0.000000000000000000 ) ) ;
#12331=AXIS2_PLACEMENT_3D ( 'NONE', #6642, #3328, #8390 ) ;
#12332=VECTOR ( 'NONE', #410, 1000.000000000000000 ) ;
#12334=DIRECTION ( 'NONE',  ( 0.000000000000000000, 0.000000000000000000, 1.000000000000000000 ) ) ;
#12343=VECTOR ( 'NONE', #17735, 1000.000000000000000 ) ;
#12344=VERTEX_POINT ( 'NONE', #11308 ) ;
#12352=AXIS2_PLACEMENT_3D ( 'NONE', #19940, #8624, #10388 ) ;
#12354=CARTESIAN_POINT ( 'NONE',  ( -3.795335389125411904E-15, 146.8256012863087676, 480.6843163258853906 ) ) ;
#12364=( NAMED_UNIT ( * ) PLANE_ANGLE_UNIT ( ) SI_UNIT ( $, .RADIAN. ) );
#12369=LINE ( 'NONE', #19868, #7949 ) ;
#12373=VERTEX_POINT ( 'NONE', #19936 ) ;
#12381=UNCERTAINTY_MEASURE_WITH_UNIT (LENGTH_MEASURE( 1.000000000000000082E-05 ), #7295, 'distance_accuracy_value', 'NONE');
#12391=SURFACE_SIDE_STYLE ('',( #1533 ) ) ;
#12394=CARTESIAN_POINT ( 'NONE',  ( -38.50085094405407204, 175.4489062796178871, 505.3921618609452935 ) ) ;
#12397=MECHANICAL_DESIGN_GEOMETRIC_PRESENTATION_REPRESENTATION('',(#1171),#11077);
#12412=DIRECTION ( 'NONE',  ( -1.000000000000000000, 0.000000000000000000, 7.715811803773179210E-14 ) ) ;
#12419=PLANE ( 'NONE',  #14612 ) ;
#12422=( LENGTH_UNIT ( ) NAMED_UNIT ( * ) SI_UNIT ( .MILLI., .METRE. ) );
#12427=DIRECTION ( 'NONE',  ( 1.000000000000000000, 0.000000000000000000, 0.000000000000000000 ) ) ;
#12428=ADVANCED_FACE ( 'NONE', ( #4205 ), #16687, .T. ) ;
#12429=VERTEX_POINT ( 'NONE', #13767 ) ;
#12433=CIRCLE ( 'NONE', #6191, 9.000000000000007105 ) ;
#12435=DIRECTION ( 'NONE',  ( 0.000000000000000000, 0.000000000000000000, -1.000000000000000000 ) ) ;
#12437=CYLINDRICAL_SURFACE ( 'NONE', #9825, 1.000000000000000888 ) ;
#12444=CIRCLE ( 'NONE', #6516, 8.000000000000007105 ) ;
#12445=EDGE_LOOP ( 'NONE', ( #6218, #4553, #9022, #12614 ) ) ;
#12446=EDGE_CURVE ( 'NONE', #16969, #1878, #7891, .T. ) ;
#12451=DIRECTION ( 'NONE',  ( 1.000000000000000000, 0.000000000000000000, -0.000000000000000000 ) ) ;
#12462=DIRECTION ( 'NONE',  ( 8.479266908829339085E-16, -1.000000000000000000, 0.000000000000000000 ) ) ;
#12466=CARTESIAN_POINT ( 'NONE',  ( -38.50085094405407204, 159.0821755739672483, 510.3921618609452935 ) ) ;
#12473=ORIENTED_EDGE ( 'NONE', *, *, #2158, .F. ) ;
#12475=ORIENTED_EDGE ( 'NONE', *, *, #12255, .T. ) ;
#12478=LINE ( 'NONE', #15700, #1972 ) ;
#12480=FACE_OUTER_BOUND ( 'NONE', #16489, .T. ) ;
#12481=FACE_OUTER_BOUND ( 'NONE', #13201, .T. ) ;
#12482=SURFACE_STYLE_USAGE ( .BOTH. , #4549 ) ;
#12487=EDGE_CURVE ( 'NONE', #19036, #19368, #9681, .T. ) ;
#12489=CIRCLE ( 'NONE', #6902, 0.9999999999999964473 ) ;
#12490=LINE ( 'NONE', #1853, #15637 ) ;
#12502=CARTESIAN_POINT ( 'NONE',  ( 0.2098432949449543505, 140.7834779774802030, 501.2072179691460292 ) ) ;
#12503=DIRECTION ( 'NONE',  ( 1.000000000000000000, 0.000000000000000000, 0.000000000000000000 ) ) ;
#12517=ORIENTED_EDGE ( 'NONE', *, *, #16803, .F. ) ;
#12525=ADVANCED_FACE ( 'NONE', ( #11591 ), #3771, .T. ) ;
#12526=AXIS2_PLACEMENT_3D ( 'NONE', #8656, #13505, #5560 ) ;
#12549=CARTESIAN_POINT ( 'NONE',  ( -79.21172376363730905, 140.1316991070070515, 501.4510136243916918 ) ) ;
#12553=FACE_OUTER_BOUND ( 'NONE', #7301, .T. ) ;
#12554=EDGE_LOOP ( 'NONE', ( #12836, #5573, #5249, #8019 ) ) ;
#12556=DIRECTION ( 'NONE',  ( -0.000000000000000000, -1.000000000000000000, -0.000000000000000000 ) ) ;
#12557=AXIS2_PLACEMENT_3D ( 'NONE', #7447, #13915, #10729 ) ;
#12568=CIRCLE ( 'NONE', #11579, 1.000000000000000888 ) ;
#12569=EDGE_LOOP ( 'NONE', ( #18742, #15694, #19906, #342 ) ) ;
#12570=CARTESIAN_POINT ( 'NONE',  ( -82.18192946989108805, 139.7703989349477354, 489.5655098179820470 ) ) ;
#12571=AXIS2_PLACEMENT_3D ( 'NONE', #7813, #15664, #12451 ) ;
#12582=VECTOR ( 'NONE', #4105, 1000.000000000000000 ) ;
#12586=CARTESIAN_POINT ( 'NONE',  ( -0.6989004220145259572, 140.0033368016316899, 501.2452398760866004 ) ) ;
#12589=CARTESIAN_POINT ( 'NONE',  ( -82.18192946989275072, 140.4048636633015406, 499.8237260975782306 ) ) ;
#12596=VERTEX_POINT ( 'NONE', #8308 ) ;
#12598=ORIENTED_EDGE ( 'NONE', *, *, #6284, .F. ) ;
#12599=DIRECTION ( 'NONE',  ( 0.000000000000000000, 0.000000000000000000, -1.000000000000000000 ) ) ;
#12603=CARTESIAN_POINT ( 'NONE',  ( 0.9274145758904028813, 140.4048636662046476, 500.8237260975781737 ) ) ;
#12604=DIRECTION ( 'NONE',  ( 0.000000000000000000, 0.000000000000000000, 1.000000000000000000 ) ) ;
#12611=SURFACE_STYLE_USAGE ( .BOTH. , #6332 ) ;
#12614=ORIENTED_EDGE ( 'NONE', *, *, #17421, .T. ) ;
#12622=DIRECTION ( 'NONE',  ( 1.000000000000000000, 0.000000000000000000, 0.000000000000000000 ) ) ;
#12630=ADVANCED_FACE ( 'NONE', ( #457 ), #6669, .T. ) ;
#12634=FACE_OUTER_BOUND ( 'NONE', #13695, .T. ) ;
#12637=CIRCLE ( 'NONE', #3751, 8.000000000000007105 ) ;
#12638=( NAMED_UNIT ( * ) SI_UNIT ( $, .STERADIAN. ) SOLID_ANGLE_UNIT ( ) );
#12640=ADVANCED_FACE ( 'NONE', ( #5127 ), #11397, .F. ) ;
#12644=DIRECTION ( 'NONE',  ( 0.000000000000000000, 1.000000000000000000, -0.000000000000000000 ) ) ;
#12648=CARTESIAN_POINT ( 'NONE',  ( -0.3790084242192233166, 138.8315893944087804, 489.8888383420726313 ) ) ;
#12649=ORIENTED_EDGE ( 'NONE', *, *, #14197, .F. ) ;
#12656=VECTOR ( 'NONE', #18514, 1000.000000000000000 ) ;
#12659=CARTESIAN_POINT ( 'NONE',  ( -79.41690675704376190, 139.9142446525435730, 501.0853735595708258 ) ) ;
#12666=CARTESIAN_POINT ( 'NONE',  ( -64.99999999999995737, 316.7545334744432353, 495.1946179577816451 ) ) ;
#12667=COLOUR_RGB ( '', 0.31764706, 0.68627451, 0.89019608) ;
#12674=CARTESIAN_POINT ( 'NONE',  ( 0.9999999999997842837, 140.4048636633015406, 499.8237260975782306 ) ) ;
#12675=( GEOMETRIC_REPRESENTATION_CONTEXT ( 3 ) GLOBAL_UNCERTAINTY_ASSIGNED_CONTEXT ( ( #8701 ) ) GLOBAL_UNIT_ASSIGNED_CONTEXT ( ( #6096, #6400, #10818 ) ) REPRESENTATION_CONTEXT ( 'NONE', 'WORKASPACE' ) );
#12679=ADVANCED_FACE ( 'NONE', ( #8499 ), #4778, .T. ) ;
#12680=DIRECTION ( 'NONE',  ( -1.000000000000000000, 0.000000000000000000, 0.000000000000000000 ) ) ;
#12691=ORIENTED_EDGE ( 'NONE', *, *, #14197, .T. ) ;
#12702=CYLINDRICAL_SURFACE ( 'NONE', #19825, 3.883636366625808911 ) ;
#12703=AXIS2_PLACEMENT_3D ( 'NONE', #5802, #13821, #16827 ) ;
#12707=DIRECTION ( 'NONE',  ( 0.000000000000000000, 1.000000000000000000, -0.000000000000000000 ) ) ;
#12723=CARTESIAN_POINT ( 'NONE',  ( -0.08504567063205197008, 140.3618719181226879, 501.8057946578301198 ) ) ;
#12724=FACE_OUTER_BOUND ( 'NONE', #12808, .T. ) ;
#12726=CARTESIAN_POINT ( 'NONE',  ( -79.99999999999995737, 219.7545334744432921, 512.1946179577817020 ) ) ;
#12736=SURFACE_STYLE_FILL_AREA ( #4796 ) ;
#12745=CARTESIAN_POINT ( 'NONE',  ( -81.00000000000127898, 139.7703989349477354, 489.5655098179835818 ) ) ;
#12756=DIRECTION ( 'NONE',  ( 3.968396791731440098E-12, 0.000000000000000000, -1.000000000000000000 ) ) ;
#12757=LINE ( 'NONE', #4702, #19487 ) ;
#12758=CARTESIAN_POINT ( 'NONE',  ( -0.5568521349156368982, 138.8628622585138430, 489.6726277272926495 ) ) ;
#12770=EDGE_CURVE ( 'NONE', #19819, #12373, #18065, .T. ) ;
#12781=DIRECTION ( 'NONE',  ( -1.135258727068399668E-15, 0.000000000000000000, 1.000000000000000000 ) ) ;
#12790=ORIENTED_EDGE ( 'NONE', *, *, #2858, .T. ) ;
#12791=DIRECTION ( 'NONE',  ( 1.000000000000000000, 0.000000000000000000, 0.000000000000000000 ) ) ;
#12802=ORIENTED_EDGE ( 'NONE', *, *, #3599, .F. ) ;
#12805=AXIS2_PLACEMENT_3D ( 'NONE', #17436, #3137, #17138 ) ;
#12808=EDGE_LOOP ( 'NONE', ( #3554, #14004, #18258, #2950 ) ) ;
#12810=ORIENTED_EDGE ( 'NONE', *, *, #8535, .T. ) ;
#12816=CARTESIAN_POINT ( 'NONE',  ( 1.181929469892980755, 139.7545334744432637, 496.6642397995874489 ) ) ;
#12819=CARTESIAN_POINT ( 'NONE',  ( -1.214306433183764966E-14, 141.6406393683235194, 501.8237260975781737 ) ) ;
#12823=DIRECTION ( 'NONE',  ( 0.000000000000000000, 0.000000000000000000, 1.000000000000000000 ) ) ;
#12827=CARTESIAN_POINT ( 'NONE',  ( -82.18192946989245229, 139.7545334744432637, 491.0690926367355473 ) ) ;
#12836=ORIENTED_EDGE ( 'NONE', *, *, #19459, .T. ) ;
#12843=CARTESIAN_POINT ( 'NONE',  ( -78.99999999999995737, 138.7545334744432637, 510.3921618609452935 ) ) ;
#12855=CARTESIAN_POINT ( 'NONE',  ( -78.99999999999995737, 216.7545334744432921, 477.3411705753777596 ) ) ;
#12861=ORIENTED_EDGE ( 'NONE', *, *, #12770, .F. ) ;
#12867=ORIENTED_EDGE ( 'NONE', *, *, #9245, .T. ) ;
#12869=CARTESIAN_POINT ( 'NONE',  ( -79.15851041973368751, 140.2141937887648453, 501.5802637535626900 ) ) ;
#12880=DIRECTION ( 'NONE',  ( 3.328238341717372086E-14, 0.000000000000000000, -1.000000000000000000 ) ) ;
#12886=ORIENTED_EDGE ( 'NONE', *, *, #10033, .F. ) ;
#12896=AXIS2_PLACEMENT_3D ( 'NONE', #4533, #13604, #10812 ) ;
#12897=VECTOR ( 'NONE', #18442, 1000.000000000000000 ) ;
#12911=AXIS2_PLACEMENT_3D ( 'NONE', #5428, #6882, #17687 ) ;
#12912=EDGE_CURVE ( 'NONE', #1482, #8271, #18570, .T. ) ;
#12919=AXIS2_PLACEMENT_3D ( 'NONE', #3551, #9831, #441 ) ;
#12922=DIRECTION ( 'NONE',  ( 0.000000000000000000, -0.000000000000000000, -1.000000000000000000 ) ) ;
#12933=CARTESIAN_POINT ( 'NONE',  ( -15.00000000000000000, 317.7545334744432353, 475.1454018718993098 ) ) ;
#12936=EDGE_CURVE ( 'NONE', #19489, #18686, #19888, .T. ) ;
#12941=AXIS2_PLACEMENT_3D ( 'NONE', #3991, #2638, #16583 ) ;
#12953=CARTESIAN_POINT ( 'NONE',  ( -1.273471684549477371E-14, 140.0803823864558808, 488.6808193230643269 ) ) ;
#12956=CIRCLE ( 'NONE', #13916, 1.000000000000000888 ) ;
#12957=DIRECTION ( 'NONE',  ( 0.000000000000000000, -1.632680918566406793E-16, 1.000000000000000000 ) ) ;
#12960=CARTESIAN_POINT ( 'NONE',  ( -81.18192946989242387, 138.7545334744432637, 490.5655098179833544 ) ) ;
#12964=CARTESIAN_POINT ( 'NONE',  ( -82.18192946989263703, 147.7545334744432921, 496.6642397995873921 ) ) ;
#12972=ADVANCED_FACE ( 'NONE', ( #543 ), #16134, .F. ) ;
#12981=DIRECTION ( 'NONE',  ( -0.000000000000000000, -1.000000000000000000, -1.632680918566406547E-16 ) ) ;
#12983=FACE_OUTER_BOUND ( 'NONE', #15152, .T. ) ;
#12985=VECTOR ( 'NONE', #14405, 1000.000000000000000 ) ;
#13004=MECHANICAL_DESIGN_GEOMETRIC_PRESENTATION_REPRESENTATION('',(#13642),#18234);
#13005=LINE ( 'NONE', #19275, #14293 ) ;
#13006=AXIS2_PLACEMENT_3D ( 'NONE', #1630, #15796, #1536 ) ;
#13033=DIRECTION ( 'NONE',  ( -0.000000000000000000, -1.000000000000000000, -0.000000000000000000 ) ) ;
#13041=ADVANCED_FACE ( 'NONE', ( #9599 ), #15921, .F. ) ;
#13042=CARTESIAN_POINT ( 'NONE',  ( -38.50085094405407204, 175.4489062796178871, 510.3921618609452935 ) ) ;
#13043=CARTESIAN_POINT ( 'NONE',  ( -82.18192946989263703, 139.7545334744432637, 496.6642397995874489 ) ) ;
#13050=CARTESIAN_POINT ( 'NONE',  ( -79.99999999999995737, 138.7545334744432637, 510.3921618609452935 ) ) ;
#13057=ORIENTED_EDGE ( 'NONE', *, *, #435, .F. ) ;
#13060=DIRECTION ( 'NONE',  ( 0.000000000000000000, 0.000000000000000000, -1.000000000000000000 ) ) ;
#13063=UNCERTAINTY_MEASURE_WITH_UNIT (LENGTH_MEASURE( 1.000000000000000082E-05 ), #16258, 'distance_accuracy_value', 'NONE');
#13066=AXIS2_PLACEMENT_3D ( 'NONE', #9836, #19209, #10426 ) ;
#13067=ORIENTED_EDGE ( 'NONE', *, *, #11818, .T. ) ;
#13073=CARTESIAN_POINT ( 'NONE',  ( -15.00000000000000000, 317.7545334744432353, 475.1454018718993098 ) ) ;
#13077=CARTESIAN_POINT ( 'NONE',  ( -79.99999999999995737, 147.7545334744432921, 496.6642397995874489 ) ) ;
#13089=ORIENTED_EDGE ( 'NONE', *, *, #16949, .F. ) ;
#13090=DIRECTION ( 'NONE',  ( 0.000000000000000000, 0.7071067811865336949, -0.7071067811865614505 ) ) ;
#13109=ORIENTED_EDGE ( 'NONE', *, *, #1969, .F. ) ;
#13113=FACE_OUTER_BOUND ( 'NONE', #9964, .T. ) ;
#13119=DIRECTION ( 'NONE',  ( 0.000000000000000000, 0.000000000000000000, -1.000000000000000000 ) ) ;
#13122=DIRECTION ( 'NONE',  ( 7.714098457234357737E-14, 0.000000000000000000, 1.000000000000000000 ) ) ;
#13123=LINE ( 'NONE', #2159, #12332 ) ;
#13137=DIRECTION ( 'NONE',  ( 0.000000000000000000, 0.000000000000000000, 1.000000000000000000 ) ) ;
#13146=ORIENTED_EDGE ( 'NONE', *, *, #13879, .T. ) ;
#13155=DIRECTION ( 'NONE',  ( -1.000000000000000000, 0.000000000000000000, 0.000000000000000000 ) ) ;
#13160=SURFACE_STYLE_USAGE ( .BOTH. , #19320 ) ;
#13171=EDGE_CURVE ( 'NONE', #11471, #17234, #5806, .T. ) ;
#13186=CYLINDRICAL_SURFACE ( 'NONE', #12293, 1.000000000000000888 ) ;
#13194=ORIENTED_EDGE ( 'NONE', *, *, #4218, .F. ) ;
#13201=EDGE_LOOP ( 'NONE', ( #11692, #12108, #11578, #11656 ) ) ;
#13216=EDGE_CURVE ( 'NONE', #3885, #14143, #17506, .T. ) ;
#13218=AXIS2_PLACEMENT_3D ( 'NONE', #7938, #1523, #11039 ) ;
#13227=CARTESIAN_POINT ( 'NONE',  ( -78.99999999999995737, 152.4824555358011082, 478.3411705753777596 ) ) ;
#13236=PLANE ( 'NONE',  #13946 ) ;
#13252=CARTESIAN_POINT ( 'NONE',  ( -64.99999999999995737, 317.7545334744432353, 475.1454018718993098 ) ) ;
#13263=ORIENTED_EDGE ( 'NONE', *, *, #14666, .T. ) ;
#13266=ORIENTED_EDGE ( 'NONE', *, *, #13879, .F. ) ;
#13274=DIRECTION ( 'NONE',  ( 0.000000000000000000, 1.000000000000000000, -0.000000000000000000 ) ) ;
#13276=TOROIDAL_SURFACE ( 'NONE', #4373, 8.000000000000000000, 1.000000000000000000 ) ;
#13282=AXIS2_PLACEMENT_3D ( 'NONE', #7125, #19157, #5265 ) ;
#13292=EDGE_CURVE ( 'NONE', #1728, #3836, #4690, .T. ) ;
#13310=SURFACE_SIDE_STYLE ('',( #14833 ) ) ;
#13311=LINE ( 'NONE', #12214, #16271 ) ;
#13313=CARTESIAN_POINT ( 'NONE',  ( -79.24209493944616156, 138.9131563295584044, 489.3642818721078243 ) ) ;
#13335=DIRECTION ( 'NONE',  ( 1.000000000000000000, -0.000000000000000000, -7.715811803773179210E-14 ) ) ;
#13337=DIRECTION ( 'NONE',  ( 0.000000000000000000, 1.000000000000000000, -0.000000000000000000 ) ) ;
#13357=MECHANICAL_DESIGN_GEOMETRIC_PRESENTATION_REPRESENTATION('',(#8723),#11693);
#13359=ORIENTED_EDGE ( 'NONE', *, *, #12250, .F. ) ;
#13398=( NAMED_UNIT ( * ) SI_UNIT ( $, .STERADIAN. ) SOLID_ANGLE_UNIT ( ) );
#13407=PRESENTATION_STYLE_ASSIGNMENT (( #17813 ) ) ;
#13409=DIRECTION ( 'NONE',  ( -0.000000000000000000, 1.000000000000000000, -0.000000000000000000 ) ) ;
#13418=DIRECTION ( 'NONE',  ( 0.000000000000000000, 0.7071067811865336949, -0.7071067811865614505 ) ) ;
#13424=EDGE_LOOP ( 'NONE', ( #643, #18312, #17868, #8403 ) ) ;
#13426=ORIENTED_EDGE ( 'NONE', *, *, #17711, .F. ) ;
#13448=ORIENTED_EDGE ( 'NONE', *, *, #5362, .T. ) ;
#13451=ORIENTED_EDGE ( 'NONE', *, *, #5273, .F. ) ;
#13455=ORIENTED_EDGE ( 'NONE', *, *, #2322, .F. ) ;
#13468=EDGE_LOOP ( 'NONE', ( #11612, #15410, #9589, #769 ) ) ;
#13480=AXIS2_PLACEMENT_3D ( 'NONE', #16335, #19070, #3637 ) ;
#13484=CARTESIAN_POINT ( 'NONE',  ( -1.000000000000009104, 141.3905724437643414, 484.7051316060566819 ) ) ;
#13493=EDGE_CURVE ( 'NONE', #15757, #2216, #2642, .T. ) ;
#13501=LINE ( 'NONE', #3823, #7135 ) ;
#13505=DIRECTION ( 'NONE',  ( -1.000000000000000000, 0.000000000000000000, 0.000000000000000000 ) ) ;
#13515=VERTEX_POINT ( 'NONE', #14924 ) ;
#13519=COLOUR_RGB ( '', 0.08235294, 0.09019608, 0.10196078) ;
#13520=DIRECTION ( 'NONE',  ( -1.000000000000000000, 0.000000000000000000, 0.000000000000000000 ) ) ;
#13523=ADVANCED_FACE ( 'NONE', ( #9039 ), #16988, .F. ) ;
#13527=CARTESIAN_POINT ( 'NONE',  ( -80.71908396425561705, 138.8395222545321133, 489.5364562303509501 ) ) ;
#13528=EDGE_LOOP ( 'NONE', ( #7673, #372, #41, #7624 ) ) ;
#13530=DIRECTION ( 'NONE',  ( -1.962615573354755500E-14, -0.7071067811865614505, -0.7071067811865336949 ) ) ;
#13535=EDGE_CURVE ( 'NONE', #15750, #368, #9537, .T. ) ;
#13542=CARTESIAN_POINT ( 'NONE',  ( -79.03224866309057006, 140.4930333293738727, 501.9895992312876274 ) ) ;
#13544=CARTESIAN_POINT ( 'NONE',  ( -21.85283368562565443, 319.7545334744432353, 489.0536462814662855 ) ) ;
#13548=FILL_AREA_STYLE_COLOUR ( '', #12143 ) ;
#13549=CARTESIAN_POINT ( 'NONE',  ( -78.99999999999995737, 152.4824555358010798, 501.3921618609452366 ) ) ;
#13559=ORIENTED_EDGE ( 'NONE', *, *, #4504, .T. ) ;
#13565=CARTESIAN_POINT ( 'NONE',  ( -1.242741617435013737E-14, 141.6406393683235194, 501.8237260975781737 ) ) ;
#13569=TOROIDAL_SURFACE ( 'NONE', #18480, 8.000000000000000000, 1.000000000000000000 ) ;
#13570=DIRECTION ( 'NONE',  ( 8.479266908829339085E-16, -1.000000000000000000, 0.000000000000000000 ) ) ;
#13577=LINE ( 'NONE', #10172, #8736 ) ;
#13582=VECTOR ( 'NONE', #12556, 1000.000000000000000 ) ;
#13590=CARTESIAN_POINT ( 'NONE',  ( -79.99999999999995737, 216.7545334744432921, 488.5655098179835818 ) ) ;
#13595=CARTESIAN_POINT ( 'NONE',  ( -79.99999999999995737, 316.7545334744432921, 155.1946179577816167 ) ) ;
#13600=FACE_OUTER_BOUND ( 'NONE', #5815, .T. ) ;
#13604=DIRECTION ( 'NONE',  ( -1.000000000000000000, 0.000000000000000000, 1.450371633464475582E-15 ) ) ;
#13607=EDGE_LOOP ( 'NONE', ( #16929, #14548, #15830, #3453 ) ) ;
#13608=DIRECTION ( 'NONE',  ( 1.450371633464484259E-15, 5.551115123125816150E-14, 1.000000000000000000 ) ) ;
#13614=AXIS2_PLACEMENT_3D ( 'NONE', #3820, #16405, #14827 ) ;
#13621=FACE_OUTER_BOUND ( 'NONE', #5354, .T. ) ;
#13622=CARTESIAN_POINT ( 'NONE',  ( -80.33253491209451624, 139.8177930281376291, 489.3130425433099049 ) ) ;
#13627=AXIS2_PLACEMENT_3D ( 'NONE', #1911, #15990, #19341 ) ;
#13633=VECTOR ( 'NONE', #13033, 1000.000000000000000 ) ;
#13642=STYLED_ITEM ( 'NONE', ( #103 ), #15010 ) ;
#13647=DIRECTION ( 'NONE',  ( -1.000000000000000000, 0.000000000000000000, 0.000000000000000000 ) ) ;
#13656=SHAPE_DEFINITION_REPRESENTATION ( #14031, #16721 ) ;
#13657=TOROIDAL_SURFACE ( 'NONE', #9049, 8.000000000000000000, 1.000000000000000000 ) ;
#13666=EDGE_CURVE ( 'NONE', #18338, #6397, #12757, .T. ) ;
#13689=DIRECTION ( 'NONE',  ( 0.000000000000000000, 0.000000000000000000, -1.000000000000000000 ) ) ;
#13692=VERTEX_POINT ( 'NONE', #3366 ) ;
#13694=ORIENTED_EDGE ( 'NONE', *, *, #12770, .T. ) ;
#13695=EDGE_LOOP ( 'NONE', ( #107, #16809, #4490, #2926 ) ) ;
#13696=EDGE_CURVE ( 'NONE', #305, #3170, #12956, .T. ) ;
#13697=CARTESIAN_POINT ( 'NONE',  ( -79.72263070831506582, 138.8189518926663482, 489.9905112626940422 ) ) ;
#13698=ORIENTED_EDGE ( 'NONE', *, *, #473, .F. ) ;
#13703=DIRECTION ( 'NONE',  ( 1.000000000000000000, 0.000000000000000000, 3.328238341717381552E-14 ) ) ;
#13717=ORIENTED_EDGE ( 'NONE', *, *, #8591, .T. ) ;
#13740=DIRECTION ( 'NONE',  ( 0.000000000000000000, 0.000000000000000000, 1.000000000000000000 ) ) ;
#13744=( NAMED_UNIT ( * ) SI_UNIT ( $, .STERADIAN. ) SOLID_ANGLE_UNIT ( ) );
#13751=ORIENTED_EDGE ( 'NONE', *, *, #14628, .F. ) ;
#13756=EDGE_LOOP ( 'NONE', ( #15712, #1589, #4797, #999 ) ) ;
#13757=CARTESIAN_POINT ( 'NONE',  ( -44.50085094405407915, 159.0821755739672483, 505.3921618609452935 ) ) ;
#13763=( NAMED_UNIT ( * ) SI_UNIT ( $, .STERADIAN. ) SOLID_ANGLE_UNIT ( ) );
#13767=CARTESIAN_POINT ( 'NONE',  ( -1.000000000000007550, 146.1184945051222428, 479.9772095446988374 ) ) ;
#13787=ORIENTED_EDGE ( 'NONE', *, *, #9857, .T. ) ;
#13797=EDGE_CURVE ( 'NONE', #11717, #17622, #5696, .T. ) ;
#13805=FACE_BOUND ( 'NONE', #16262, .T. ) ;
#13811=CARTESIAN_POINT ( 'NONE',  ( -118.0000000000000284, 316.7545334744432921, 205.1946179577815883 ) ) ;
#13817=LINE ( 'NONE', #18249, #1733 ) ;
#13820=LINE ( 'NONE', #20197, #1051 ) ;
#13821=DIRECTION ( 'NONE',  ( 1.000000000000000000, 0.000000000000000000, 0.000000000000000000 ) ) ;
#13822=LINE ( 'NONE', #2586, #13909 ) ;
#13823=CARTESIAN_POINT ( 'NONE',  ( -0.8168643132833559584, 140.1532854590085435, 501.4923746928197943 ) ) ;
#13838=CIRCLE ( 'NONE', #17452, 3.000000000000002665 ) ;
#13839=CARTESIAN_POINT ( 'NONE',  ( -79.99999999999994316, 141.4904453270995646, 501.7347375422862683 ) ) ;
#13846=ORIENTED_EDGE ( 'NONE', *, *, #2291, .T. ) ;
#13847=FACE_OUTER_BOUND ( 'NONE', #10257, .T. ) ;
#13853=AXIS2_PLACEMENT_3D ( 'NONE', #2562, #19865, #13418 ) ;
#13854=VERTEX_POINT ( 'NONE', #3845 ) ;
#13857=MECHANICAL_DESIGN_GEOMETRIC_PRESENTATION_REPRESENTATION('',(#5961),#4032);
#13860=CARTESIAN_POINT ( 'NONE',  ( 0.000000000000000000, 138.7545334744432637, 500.3921618609452366 ) ) ;
#13866=EDGE_CURVE ( 'NONE', #14767, #10724, #7989, .T. ) ;
#13868=CARTESIAN_POINT ( 'NONE',  ( -44.50085094405410757, 209.4098724938429541, 505.3921618609452935 ) ) ;
#13870=CARTESIAN_POINT ( 'NONE',  ( -79.99999999999995737, 152.4824555358010798, 501.3921618609452366 ) ) ;
#13871=AXIS2_PLACEMENT_3D ( 'NONE', #16372, #11406, #3776 ) ;
#13879=EDGE_CURVE ( 'NONE', #7546, #15663, #14859, .T. ) ;
#13891=SURFACE_STYLE_USAGE ( .BOTH. , #18523 ) ;
#13896=FACE_OUTER_BOUND ( 'NONE', #11535, .T. ) ;
#13906=MECHANICAL_DESIGN_GEOMETRIC_PRESENTATION_REPRESENTATION('',(#8980),#16562);
#13908=ORIENTED_EDGE ( 'NONE', *, *, #2838, .T. ) ;
#13909=VECTOR ( 'NONE', #12274, 1000.000000000000000 ) ;
#13915=DIRECTION ( 'NONE',  ( 1.025567617263343161E-15, 0.7071067811865455743, 0.7071067811865494601 ) ) ;
#13916=AXIS2_PLACEMENT_3D ( 'NONE', #1806, #8116, #14388 ) ;
#13927=VERTEX_POINT ( 'NONE', #5578 ) ;
#13931=EDGE_CURVE ( 'NONE', #305, #9522, #13817, .T. ) ;
#13944=DIRECTION ( 'NONE',  ( 0.000000000000000000, 0.000000000000000000, 1.000000000000000000 ) ) ;
#13946=AXIS2_PLACEMENT_3D ( 'NONE', #13050, #17660, #5098 ) ;
#13959=ORIENTED_EDGE ( 'NONE', *, *, #11088, .F. ) ;
#13964=ORIENTED_EDGE ( 'NONE', *, *, #15255, .T. ) ;
#13971=ORIENTED_EDGE ( 'NONE', *, *, #15614, .T. ) ;
#13980=SURFACE_SIDE_STYLE ('',( #2937 ) ) ;
#13982=AXIS2_PLACEMENT_3D ( 'NONE', #13549, #751, #12011 ) ;
#13990=CARTESIAN_POINT ( 'NONE',  ( -0.7691948703060754733, 138.9269458084811788, 489.3115405995010292 ) ) ;
#13993=( GEOMETRIC_REPRESENTATION_CONTEXT ( 3 ) GLOBAL_UNCERTAINTY_ASSIGNED_CONTEXT ( ( #6845 ) ) GLOBAL_UNIT_ASSIGNED_CONTEXT ( ( #7124, #2887, #9176 ) ) REPRESENTATION_CONTEXT ( 'NONE', 'WORKASPACE' ) );
#13995=ORIENTED_EDGE ( 'NONE', *, *, #11745, .T. ) ;
#14004=ORIENTED_EDGE ( 'NONE', *, *, #13171, .F. ) ;
#14008=PLANE ( 'NONE',  #3214 ) ;
#14019=CIRCLE ( 'NONE', #7118, 1.000000000000000888 ) ;
#14022=ORIENTED_EDGE ( 'NONE', *, *, #6617, .T. ) ;
#14027=DIRECTION ( 'NONE',  ( -0.000000000000000000, -0.000000000000000000, -1.000000000000000000 ) ) ;
#14030=CARTESIAN_POINT ( 'NONE',  ( -1.000000000000011768, 141.3905724437643414, 503.0282008302663144 ) ) ;
#14031=PRODUCT_DEFINITION_SHAPE ( 'NONE', 'NONE',  #5698 ) ;
#14032=ORIENTED_EDGE ( 'NONE', *, *, #3039, .F. ) ;
#14037=CARTESIAN_POINT ( 'NONE',  ( 0.000000000000000000, 216.7545334744432921, 495.1946179577816451 ) ) ;
#14050=AXIS2_PLACEMENT_3D ( 'NONE', #16382, #18082, #13090 ) ;
#14052=SURFACE_SIDE_STYLE ('',( #7772 ) ) ;
#14054=CARTESIAN_POINT ( 'NONE',  ( 0.4336145047205204883, 139.5236339024991423, 500.3048018832922708 ) ) ;
#14058=ORIENTED_EDGE ( 'NONE', *, *, #11891, .T. ) ;
#14060=DIRECTION ( 'NONE',  ( 1.000000000000000000, 0.000000000000000000, -0.000000000000000000 ) ) ;
#14071=ORIENTED_EDGE ( 'NONE', *, *, #9503, .T. ) ;
#14073=CARTESIAN_POINT ( 'NONE',  ( -79.99999999999995737, 140.0803381460330002, 488.6808864560385359 ) ) ;
#14077=ADVANCED_FACE ( 'NONE', ( #12480 ), #20089, .T. ) ;
#14083=DIRECTION ( 'NONE',  ( 1.000000000000000000, 0.000000000000000000, 0.000000000000000000 ) ) ;
#14084=CARTESIAN_POINT ( 'NONE',  ( 0.05802186526201238287, 138.7922706605886276, 490.2433561606925423 ) ) ;
#14091=DIRECTION ( 'NONE',  ( 3.295974604355930324E-14, 0.000000000000000000, -1.000000000000000000 ) ) ;
#14100=DIRECTION ( 'NONE',  ( 0.000000000000000000, 0.000000000000000000, 1.000000000000000000 ) ) ;
#14104=DIRECTION ( 'NONE',  ( 0.000000000000000000, 1.000000000000000000, 0.000000000000000000 ) ) ;
#14109=MECHANICAL_DESIGN_GEOMETRIC_PRESENTATION_REPRESENTATION('',(#14125),#5856);
#14114=FILL_AREA_STYLE_COLOUR ( '', #2100 ) ;
#14115=CARTESIAN_POINT ( 'NONE',  ( -15.00000000000000000, 317.7545334744432353, 495.1946179577816451 ) ) ;
#14119=DIRECTION ( 'NONE',  ( 0.000000000000000000, -0.000000000000000000, 1.000000000000000000 ) ) ;
#14123=CARTESIAN_POINT ( 'NONE',  ( -4.848803763073570445E-15, 146.8256012863087108, 507.0490161104376057 ) ) ;
#14125=STYLED_ITEM ( 'NONE', ( #2814 ), #11116 ) ;
#14126=CARTESIAN_POINT ( 'NONE',  ( -79.99999999999995737, 216.7545334744432921, 515.1946179577817020 ) ) ;
#14132=AXIS2_PLACEMENT_3D ( 'NONE', #8302, #1883, #11390 ) ;
#14140=CARTESIAN_POINT ( 'NONE',  ( 0.9999999999998814282, 140.4048636633015121, 500.8237260975781737 ) ) ;
#14143=VERTEX_POINT ( 'NONE', #6506 ) ;
#14144=DIRECTION ( 'NONE',  ( 0.000000000000000000, -0.9497703099767278445, -0.3129478523439812032 ) ) ;
#14148=CIRCLE ( 'NONE', #7252, 1.000000000000000444 ) ;
#14151=EDGE_LOOP ( 'NONE', ( #9422, #8193, #14796, #18028 ) ) ;
#14153=ORIENTED_EDGE ( 'NONE', *, *, #11025, .F. ) ;
#14164=CARTESIAN_POINT ( 'NONE',  ( -1.019150042136374168E-14, 152.4824555358011082, 486.3411705753778165 ) ) ;
#14165=CIRCLE ( 'NONE', #11543, 1.000000000000000888 ) ;
#14168=CARTESIAN_POINT ( 'NONE',  ( -79.99999999999995737, 138.7545334744432637, 510.3921618609452935 ) ) ;
#14188=CARTESIAN_POINT ( 'NONE',  ( -82.18192946989245229, 147.7545334744432921, 491.0690926367355473 ) ) ;
#14189=CARTESIAN_POINT ( 'NONE',  ( -78.99999999999995737, 140.8764026050587290, 502.4686618848273270 ) ) ;
#14197=EDGE_CURVE ( 'NONE', #10884, #16969, #13311, .T. ) ;
#14204=DIRECTION ( 'NONE',  ( -0.000000000000000000, -0.000000000000000000, 1.000000000000000000 ) ) ;
#14211=LINE ( 'NONE', #12570, #6425 ) ;
#14216=CARTESIAN_POINT ( 'NONE',  ( -15.00000000000000000, 316.7545334744432353, 475.1454018718993098 ) ) ;
#14226=LINE ( 'NONE', #4959, #5692 ) ;
#14229=CARTESIAN_POINT ( 'NONE',  ( -79.99999999999995737, 142.0976792249509231, 485.4122383872432351 ) ) ;
#14230=CARTESIAN_POINT ( 'NONE',  ( -21.85283368562565443, 317.7545334744432353, 489.0536462814662855 ) ) ;
#14233=VECTOR ( 'NONE', #2687, 1000.000000000000000 ) ;
#14239=ORIENTED_EDGE ( 'NONE', *, *, #978, .F. ) ;
#14243=LINE ( 'NONE', #17430, #18932 ) ;
#14246=CARTESIAN_POINT ( 'NONE',  ( 0.9999999999998516742, 139.7462607836631605, 500.8237260975782874 ) ) ;
#14247=CARTESIAN_POINT ( 'NONE',  ( -1.561251128379126385E-14, 147.7545334744432921, 491.0690926367356042 ) ) ;
#14249=ORIENTED_EDGE ( 'NONE', *, *, #11630, .F. ) ;
#14252=CIRCLE ( 'NONE', #12269, 3.000000000000016431 ) ;
#14277=FACE_OUTER_BOUND ( 'NONE', #16463, .T. ) ;
#14278=CYLINDRICAL_SURFACE ( 'NONE', #5679, 9.000000000000007105 ) ;
#14283=DIRECTION ( 'NONE',  ( 1.322943490866811299E-12, 0.000000000000000000, 1.000000000000000000 ) ) ;
#14290=AXIS2_PLACEMENT_3D ( 'NONE', #2893, #13530, #4555 ) ;
#14293=VECTOR ( 'NONE', #10289, 1000.000000000000000 ) ;
#14294=ORIENTED_EDGE ( 'NONE', *, *, #19660, .T. ) ;
#14308=CARTESIAN_POINT ( 'NONE',  ( -64.99999999999995737, 317.7545334744432353, 475.1454018718993098 ) ) ;
#14309=CARTESIAN_POINT ( 'NONE',  ( -21.85283368562565443, 319.7545334744432353, 489.0536462814662855 ) ) ;
#14329=CARTESIAN_POINT ( 'NONE',  ( -78.99999999999995737, 147.7545334744432921, 496.6642397995874489 ) ) ;
#14331=FILL_AREA_STYLE ('',( #14114 ) ) ;
#14334=AXIS2_PLACEMENT_3D ( 'NONE', #9738, #19093, #12427 ) ;
#14340=CARTESIAN_POINT ( 'NONE',  ( -21.85283368562565443, 319.7545334744432353, 481.2863735482146694 ) ) ;
#14344=CARTESIAN_POINT ( 'NONE',  ( -79.99999999999995737, 0.000000000000000000, 205.1946179577815883 ) ) ;
#14354=FACE_OUTER_BOUND ( 'NONE', #1982, .T. ) ;
#14356=VECTOR ( 'NONE', #5058, 1000.000000000000000 ) ;
#14388=DIRECTION ( 'NONE',  ( 0.000000000000000000, 0.000000000000000000, -1.000000000000000000 ) ) ;
#14391=ORIENTED_EDGE ( 'NONE', *, *, #20307, .F. ) ;
#14393=EDGE_CURVE ( 'NONE', #5490, #5074, #17620, .T. ) ;
#14394=( GEOMETRIC_REPRESENTATION_CONTEXT ( 3 ) GLOBAL_UNCERTAINTY_ASSIGNED_CONTEXT ( ( #2087 ) ) GLOBAL_UNIT_ASSIGNED_CONTEXT ( ( #20169, #12364, #7821 ) ) REPRESENTATION_CONTEXT ( 'NONE', 'WORKASPACE' ) );
#14396=LINE ( 'NONE', #11414, #10930 ) ;
#14398=ORIENTED_EDGE ( 'NONE', *, *, #16934, .T. ) ;
#14405=DIRECTION ( 'NONE',  ( 8.027491443112700323E-16, 0.7071067811865504593, -0.7071067811865445751 ) ) ;
#14425=CIRCLE ( 'NONE', #5544, 8.000000000000007105 ) ;
#14427=DIRECTION ( 'NONE',  ( 0.000000000000000000, 0.000000000000000000, 1.000000000000000000 ) ) ;
#14434=CARTESIAN_POINT ( 'NONE',  ( -79.99999999999995737, 146.8256012863087676, 507.0490161104376057 ) ) ;
#14440=ORIENTED_EDGE ( 'NONE', *, *, #3625, .F. ) ;
#14452=CARTESIAN_POINT ( 'NONE',  ( -0.5803134113676365891, 139.9120960380916188, 501.0815185958381335 ) ) ;
#14454=CARTESIAN_POINT ( 'NONE',  ( -79.99999999999995737, 316.7545334744432921, 205.1946179577815883 ) ) ;
#14455=CARTESIAN_POINT ( 'NONE',  ( -80.12104746910925712, 139.8955315650537443, 489.0596075541194523 ) ) ;
#14458=CARTESIAN_POINT ( 'NONE',  ( -44.50085094405410757, 209.4098724938429541, 510.3921618609452935 ) ) ;
#14461=CARTESIAN_POINT ( 'NONE',  ( -81.18192946989245229, 147.7545334744432921, 491.0690926367356042 ) ) ;
#14479=VECTOR ( 'NONE', #6479, 1000.000000000000000 ) ;
#14485=FACE_OUTER_BOUND ( 'NONE', #9985, .T. ) ;
#14489=VERTEX_POINT ( 'NONE', #13073 ) ;
#14494=CARTESIAN_POINT ( 'NONE',  ( -80.70993973863717486, 139.4861549367042528, 500.2186618843511496 ) ) ;
#14501=CARTESIAN_POINT ( 'NONE',  ( 0.000000000000000000, 216.7545334744432921, 515.1946179577817020 ) ) ;
#14502=FACE_OUTER_BOUND ( 'NONE', #8905, .T. ) ;
#14503=CARTESIAN_POINT ( 'NONE',  ( 0.000000000000000000, 138.7545334744432637, 510.3921618609452935 ) ) ;
#14521=FACE_OUTER_BOUND ( 'NONE', #5700, .T. ) ;
#14524=FACE_OUTER_BOUND ( 'NONE', #10719, .T. ) ;
#14534=CARTESIAN_POINT ( 'NONE',  ( -79.99999999999995737, 139.7733885855926701, 501.8237260975782874 ) ) ;
#14538=EDGE_CURVE ( 'NONE', #506, #18058, #4781, .T. ) ;
#14542=ADVANCED_FACE ( 'NONE', ( #2404 ), #1987, .T. ) ;
#14548=ORIENTED_EDGE ( 'NONE', *, *, #15391, .F. ) ;
#14553=CYLINDRICAL_SURFACE ( 'NONE', #15495, 1.000000000000000888 ) ;
#14558=DIRECTION ( 'NONE',  ( 0.000000000000000000, 0.000000000000000000, 1.000000000000000000 ) ) ;
#14559=CARTESIAN_POINT ( 'NONE',  ( 1.181929469893326257, 140.4048636633015406, 500.8237260975781737 ) ) ;
#14562=EDGE_LOOP ( 'NONE', ( #18864, #829, #10015, #10908 ) ) ;
#14565=EDGE_CURVE ( 'NONE', #9586, #19903, #16259, .T. ) ;
#14579=DIRECTION ( 'NONE',  ( 1.000000000000000000, 0.000000000000000000, -0.000000000000000000 ) ) ;
#14580=LINE ( 'NONE', #3870, #932 ) ;
#14581=DIRECTION ( 'NONE',  ( 1.000000000000000000, 0.000000000000000000, 0.000000000000000000 ) ) ;
#14584=LINE ( 'NONE', #15461, #14844 ) ;
#14601=DIRECTION ( 'NONE',  ( 0.000000000000000000, 0.000000000000000000, 1.000000000000000000 ) ) ;
#14604=( GEOMETRIC_REPRESENTATION_CONTEXT ( 3 ) GLOBAL_UNCERTAINTY_ASSIGNED_CONTEXT ( ( #5764 ) ) GLOBAL_UNIT_ASSIGNED_CONTEXT ( ( #17375, #15960, #263 ) ) REPRESENTATION_CONTEXT ( 'NONE', 'WORKASPACE' ) );
#14612=AXIS2_PLACEMENT_3D ( 'NONE', #11684, #19393, #5297 ) ;
#14622=VERTEX_POINT ( 'NONE', #10351 ) ;
#14623=TOROIDAL_SURFACE ( 'NONE', #6411, 8.000000000000000000, 1.000000000000000000 ) ;
#14628=EDGE_CURVE ( 'NONE', #18411, #15133, #6788, .T. ) ;
#14636=CARTESIAN_POINT ( 'NONE',  ( -1.274252908074454287E-14, 138.8810201506713611, 488.5655098179835818 ) ) ;
#14660=UNCERTAINTY_MEASURE_WITH_UNIT (LENGTH_MEASURE( 1.000000000000000082E-05 ), #19557, 'distance_accuracy_value', 'NONE');
#14662=LINE ( 'NONE', #9715, #509 ) ;
#14666=EDGE_CURVE ( 'NONE', #5319, #5083, #9538, .T. ) ;
#14675=CARTESIAN_POINT ( 'NONE',  ( 2.181929469892980755, 139.7545334744432637, 496.6642397995873921 ) ) ;
#14697=LINE ( 'NONE', #13252, #4557 ) ;
#14698=( NAMED_UNIT ( * ) SI_UNIT ( $, .STERADIAN. ) SOLID_ANGLE_UNIT ( ) );
#14704=EDGE_LOOP ( 'NONE', ( #6980, #6073, #12517, #20074 ) ) ;
#14706=VERTEX_POINT ( 'NONE', #10752 ) ;
#14717=CARTESIAN_POINT ( 'NONE',  ( 0.8610374118361808771, 138.8314847497733524, 489.5655098155585279 ) ) ;
#14719=CARTESIAN_POINT ( 'NONE',  ( -1.242741617435013895E-14, 216.7545334744432921, 501.8237260975781737 ) ) ;
#14720=EDGE_CURVE ( 'NONE', #18268, #13692, #2144, .T. ) ;
#14731=DIRECTION ( 'NONE',  ( 0.000000000000000000, 0.000000000000000000, -1.000000000000000000 ) ) ;
#14744=LINE ( 'NONE', #14534, #4430 ) ;
#14746=VECTOR ( 'NONE', #16982, 1000.000000000000000 ) ;
#14765=ADVANCED_FACE ( 'NONE', ( #6325 ), #16067, .T. ) ;
#14767=VERTEX_POINT ( 'NONE', #8182 ) ;
#14771=AXIS2_PLACEMENT_3D ( 'NONE', #18064, #9947, #3964 ) ;
#14773=CARTESIAN_POINT ( 'NONE',  ( 0.8615489040082175975, 139.7703989349544713, 489.5655098179837523 ) ) ;
#14778=EDGE_CURVE ( 'NONE', #18686, #4266, #4144, .T. ) ;
#14780=DIRECTION ( 'NONE',  ( 0.000000000000000000, -0.7071067811865753283, 0.7071067811865198172 ) ) ;
#14791=EDGE_LOOP ( 'NONE', ( #7972, #13751, #10425, #9743 ) ) ;
#14796=ORIENTED_EDGE ( 'NONE', *, *, #15707, .F. ) ;
#14808=CARTESIAN_POINT ( 'NONE',  ( -1.000000000000012657, 140.8764026050585869, 502.4686618848270996 ) ) ;
#14814=VERTEX_POINT ( 'NONE', #19385 ) ;
#14815=AXIS2_PLACEMENT_3D ( 'NONE', #19451, #5358, #4006 ) ;
#14817=PRODUCT_DEFINITION_CONTEXT ( 'detailed design', #17633, 'design' ) ;
#14823=CARTESIAN_POINT ( 'NONE',  ( -79.05444436839837863, 139.0463324665402070, 488.7916445138383210 ) ) ;
#14827=DIRECTION ( 'NONE',  ( 0.000000000000000000, 0.000000000000000000, 1.000000000000000000 ) ) ;
#14831=LINE ( 'NONE', #14636, #6819 ) ;
#14833=SURFACE_STYLE_FILL_AREA ( #8650 ) ;
#14838=CARTESIAN_POINT ( 'NONE',  ( -78.99999999999995737, 139.2066006846527841, 488.2525619656395861 ) ) ;
#14844=VECTOR ( 'NONE', #18643, 1000.000000000000000 ) ;
#14845=VECTOR ( 'NONE', #499, 1000.000000000000000 ) ;
#14850=VERTEX_POINT ( 'NONE', #13042 ) ;
#14859=LINE ( 'NONE', #7047, #7022 ) ;
#14873=AXIS2_PLACEMENT_3D ( 'NONE', #5442, #484, #11728 ) ;
#14875=LINE ( 'NONE', #6866, #3432 ) ;
#14880=CARTESIAN_POINT ( 'NONE',  ( 1.181929469892980755, 147.7545334744432921, 496.6642397995874489 ) ) ;
#14885=ORIENTED_EDGE ( 'NONE', *, *, #8810, .F. ) ;
#14887=CARTESIAN_POINT ( 'NONE',  ( 0.000000000000000000, 216.7545334744432921, 512.1946179577817020 ) ) ;
#14916=FACE_OUTER_BOUND ( 'NONE', #13468, .T. ) ;
#14919=ADVANCED_FACE ( 'NONE', ( #13621 ), #12086, .F. ) ;
#14921=( NAMED_UNIT ( * ) SI_UNIT ( $, .STERADIAN. ) SOLID_ANGLE_UNIT ( ) );
#14924=CARTESIAN_POINT ( 'NONE',  ( -1.000000000000012657, 139.2066006846527841, 488.2525619656395861 ) ) ;
#14926=UNCERTAINTY_MEASURE_WITH_UNIT (LENGTH_MEASURE( 1.000000000000000082E-05 ), #17213, 'distance_accuracy_value', 'NONE');
#14932=ADVANCED_FACE ( 'NONE', ( #5994 ), #11880, .T. ) ;
#14933=ORIENTED_EDGE ( 'NONE', *, *, #5362, .F. ) ;
#14937=CARTESIAN_POINT ( 'NONE',  ( -79.01070358830934026, 139.1212506049081981, 488.5223375167593076 ) ) ;
#14946=PRESENTATION_STYLE_ASSIGNMENT (( #19559 ) ) ;
#14980=AXIS2_PLACEMENT_3D ( 'NONE', #8772, #16806, #15254 ) ;
#14998=CARTESIAN_POINT ( 'NONE',  ( -78.99999999999995737, 147.7545334744432921, 491.0690926367356042 ) ) ;
#15001=VECTOR ( 'NONE', #12113, 1000.000000000000000 ) ;
#15010=MANIFOLD_SOLID_BREP ( 'Cut-Extrude1', #17219 ) ;
#15012=B_SPLINE_CURVE_WITH_KNOTS ( 'NONE', 3,
 ( #3107, #20095, #9, #13823, #12586, #10737, #15706, #2890, #5996, #15488, #6310, #10943, #12275, #9179 ),
 .UNSPECIFIED., .F., .F.,
 ( 4, 2, 2, 2, 2, 2, 4 ),
 ( 0.000000000000000000, 0.0009284677239257688175, 0.001856935447851537635, 0.002321169309814422044, 0.002785403171777306452, 0.003249637033740190861, 0.003713870895703075270 ),
 .UNSPECIFIED. ) ;
#15022=CARTESIAN_POINT ( 'NONE',  ( 0.1271853858195616527, 139.8992328697892162, 489.0579231335084955 ) ) ;
#15038=EDGE_CURVE ( 'NONE', #16331, #9586, #1310, .T. ) ;
#15040=VECTOR ( 'NONE', #16570, 1000.000000000000000 ) ;
#15044=CARTESIAN_POINT ( 'NONE',  ( 0.000000000000000000, 316.7545334744432353, 495.1946179577816451 ) ) ;
#15045=FILL_AREA_STYLE_COLOUR ( '', #9426 ) ;
#15046=CARTESIAN_POINT ( 'NONE',  ( -82.18192946989277914, 138.7545334744432637, 500.8237260975782874 ) ) ;
#15061=ORIENTED_EDGE ( 'NONE', *, *, #17944, .T. ) ;
#15068=DIRECTION ( 'NONE',  ( 1.000000000000000000, 0.000000000000000000, 0.000000000000000000 ) ) ;
#15071=( NAMED_UNIT ( * ) SI_UNIT ( $, .STERADIAN. ) SOLID_ANGLE_UNIT ( ) );
#15074=CARTESIAN_POINT ( 'NONE',  ( -81.00000000000258638, 138.7723821175183900, 490.5025619656395861 ) ) ;
#15080=CIRCLE ( 'NONE', #9464, 3.883636366625808911 ) ;
#15091=FACE_OUTER_BOUND ( 'NONE', #14704, .T. ) ;
#15099=LINE ( 'NONE', #4186, #17131 ) ;
#15101=EDGE_LOOP ( 'NONE', ( #4798, #10443, #14153, #20127 ) ) ;
#15102=PLANE ( 'NONE',  #11926 ) ;
#15103=VERTEX_POINT ( 'NONE', #19799 ) ;
#15109=DIRECTION ( 'NONE',  ( 0.000000000000000000, -0.000000000000000000, -1.000000000000000000 ) ) ;
#15122=( NAMED_UNIT ( * ) PLANE_ANGLE_UNIT ( ) SI_UNIT ( $, .RADIAN. ) );
#15126=ORIENTED_EDGE ( 'NONE', *, *, #17561, .F. ) ;
#15129=B_SPLINE_CURVE_WITH_KNOTS ( 'NONE', 3,
 ( #59, #4913, #18622, #14084, #15854, #3367, #12648, #12758, #2944, #13990, #15965, #1809, #17167, #6170 ),
 .UNSPECIFIED., .F., .F.,
 ( 4, 2, 2, 2, 2, 2, 4 ),
 ( 0.000000000000000000, 0.0008478132045734761016, 0.001271719806860251720, 0.001695626409147027447, 0.002119533011433802957, 0.002543439613720578901, 0.003391252818294112140 ),
 .UNSPECIFIED. ) ;
#15133=VERTEX_POINT ( 'NONE', #13544 ) ;
#15139=DIRECTION ( 'NONE',  ( 0.000000000000000000, 1.000000000000000000, 0.000000000000000000 ) ) ;
#15152=EDGE_LOOP ( 'NONE', ( #15347, #13455, #9008, #10555 ) ) ;
#15153=CARTESIAN_POINT ( 'NONE',  ( -58.16843972078500258, 319.7545334744432353, 485.1700099148404206 ) ) ;
#15164=ADVANCED_FACE ( 'NONE', ( #15091 ), #940, .T. ) ;
#15166=FILL_AREA_STYLE ('',( #8416 ) ) ;
#15169=CARTESIAN_POINT ( 'NONE',  ( -81.18192946989111647, 216.7545334744432921, 489.5655098179833544 ) ) ;
#15176=AXIS2_PLACEMENT_3D ( 'NONE', #16957, #7779, #14060 ) ;
#15190=CARTESIAN_POINT ( 'NONE',  ( -80.91178762245726830, 140.4048636633015690, 500.8237260975782874 ) ) ;
#15191=SURFACE_STYLE_USAGE ( .BOTH. , #10649 ) ;
#15203=ORIENTED_EDGE ( 'NONE', *, *, #10924, .T. ) ;
#15207=EDGE_CURVE ( 'NONE', #16622, #625, #18973, .T. ) ;
#15215=VECTOR ( 'NONE', #14204, 1000.000000000000000 ) ;
#15225=CARTESIAN_POINT ( 'NONE',  ( -118.0000000000000284, 316.7545334744432921, 205.1946179577815883 ) ) ;
#15244=DIRECTION ( 'NONE',  ( 0.000000000000000000, 0.000000000000000000, 1.000000000000000000 ) ) ;
#15246=DIRECTION ( 'NONE',  ( -3.328238341717372086E-14, 0.000000000000000000, 1.000000000000000000 ) ) ;
#15254=DIRECTION ( 'NONE',  ( -1.000000000000000000, 0.000000000000000000, -5.551115123125777653E-14 ) ) ;
#15255=EDGE_CURVE ( 'NONE', #19144, #1021, #10046, .T. ) ;
#15258=ORIENTED_EDGE ( 'NONE', *, *, #6657, .F. ) ;
#15272=CARTESIAN_POINT ( 'NONE',  ( -1.450371633464477160E-15, 216.7545334744432921, 509.3921618609452935 ) ) ;
#15273=ADVANCED_FACE ( 'NONE', ( #9301 ), #1758, .T. ) ;
#15275=MANIFOLD_SOLID_BREP ( 'Boss-Extrude4', #12277 ) ;
#15277=CARTESIAN_POINT ( 'NONE',  ( -80.86756541979772805, 139.7703989356676004, 489.5655098179837523 ) ) ;
#15281=ADVANCED_BREP_SHAPE_REPRESENTATION ( '', ( #8230, #15010, #15275, #8135, #2741 ), #14604 ) ;
#15291=ORIENTED_EDGE ( 'NONE', *, *, #20299, .F. ) ;
#15303=FILL_AREA_STYLE ('',( #13548 ) ) ;
#15307=DIRECTION ( 'NONE',  ( 0.000000000000000000, -0.7071067811865336949, -0.7071067811865614505 ) ) ;
#15308=CARTESIAN_POINT ( 'NONE',  ( -21.85283368562565443, 317.7545334744432353, 481.2863735482146694 ) ) ;
#15321=PLANE ( 'NONE',  #18921 ) ;
#15322=ORIENTED_EDGE ( 'NONE', *, *, #2838, .F. ) ;
#15323=CARTESIAN_POINT ( 'NONE',  ( 0.4453342799582463707, 140.5544088492690946, 500.9879276894058080 ) ) ;
#15339=( LENGTH_UNIT ( ) NAMED_UNIT ( * ) SI_UNIT ( .MILLI., .METRE. ) );
#15340=AXIS2_PLACEMENT_3D ( 'NONE', #7769, #3006, #12599 ) ;
#15347=ORIENTED_EDGE ( 'NONE', *, *, #9151, .F. ) ;
#15350=CARTESIAN_POINT ( 'NONE',  ( -79.62203884913070340, 138.8314538163270981, 489.8899081770637167 ) ) ;
#15359=VECTOR ( 'NONE', #4949, 1000.000000000000000 ) ;
#15374=CARTESIAN_POINT ( 'NONE',  ( -44.50085094405407915, 175.4489062796178871, 505.3921618609452935 ) ) ;
#15391=EDGE_CURVE ( 'NONE', #14706, #20158, #2475, .T. ) ;
#15397=CARTESIAN_POINT ( 'NONE',  ( -79.19244403447679304, 140.1600456049978618, 501.4957876295819119 ) ) ;
#15401=CARTESIAN_POINT ( 'NONE',  ( -64.99999999999995737, 317.7545334744432353, 495.1946179577816451 ) ) ;
#15410=ORIENTED_EDGE ( 'NONE', *, *, #5741, .T. ) ;
#15411=ORIENTED_EDGE ( 'NONE', *, *, #16009, .F. ) ;
#15420=EDGE_CURVE ( 'NONE', #1728, #2022, #13577, .T. ) ;
#15427=CARTESIAN_POINT ( 'NONE',  ( -80.99999999999995737, 138.7545334744432637, 501.8237260975782874 ) ) ;
#15428=ADVANCED_FACE ( 'NONE', ( #784 ), #5541, .F. ) ;
#15431=FACE_OUTER_BOUND ( 'NONE', #11918, .T. ) ;
#15444=CARTESIAN_POINT ( 'NONE',  ( -58.16843972078500258, 317.7545334744432353, 485.1700099148404206 ) ) ;
#15454=B_SPLINE_CURVE_WITH_KNOTS ( 'NONE', 3,
 ( #20250, #9217, #9021, #16866, #6153, #15323, #18697, #15530, #10669, #4588, #1351, #8828, #10872, #13565 ),
 .UNSPECIFIED., .F., .F.,
 ( 4, 2, 2, 2, 2, 2, 4 ),
 ( 0.000000000000000000, 0.0002607493764501894956, 0.0005214987529003789913, 0.0007822481293505684869, 0.001042997505800757983, 0.001564496258701136974, 0.002085995011601515965 ),
 .UNSPECIFIED. ) ;
#15455=CARTESIAN_POINT ( 'NONE',  ( -1.450371633464476962E-15, 138.7545334744432637, 509.3921618609452935 ) ) ;
#15456=CARTESIAN_POINT ( 'NONE',  ( -9.162750170181086975E-15, 142.0976792249508946, 485.4122383872432351 ) ) ;
#15461=CARTESIAN_POINT ( 'NONE',  ( -82.18192946989243808, 138.7545334744432637, 490.5655098179832976 ) ) ;
#15473=ORIENTED_EDGE ( 'NONE', *, *, #18117, .F. ) ;
#15478=CARTESIAN_POINT ( 'NONE',  ( -79.99999999999995737, 316.7545334744432353, 515.1946179577817020 ) ) ;
#15480=FACE_OUTER_BOUND ( 'NONE', #19599, .T. ) ;
#15488=CARTESIAN_POINT ( 'NONE',  ( 0.2538567052040897609, 139.5545947507227709, 500.3746700499490885 ) ) ;
#15493=AXIS2_PLACEMENT_3D ( 'NONE', #5829, #11909, #8715 ) ;
#15495=AXIS2_PLACEMENT_3D ( 'NONE', #16037, #330, #13137 ) ;
#15511=DIRECTION ( 'NONE',  ( 0.000000000000000000, -1.000000000000000000, 0.000000000000000000 ) ) ;
#15514=CARTESIAN_POINT ( 'NONE',  ( -1.135258727068400654E-15, 216.7545334744432921, 478.3411705753777596 ) ) ;
#15521=FACE_OUTER_BOUND ( 'NONE', #619, .T. ) ;
#15527=TOROIDAL_SURFACE ( 'NONE', #12896, 8.000000000000000000, 1.000000000000000000 ) ;
#15529=ORIENTED_EDGE ( 'NONE', *, *, #17144, .F. ) ;
#15530=CARTESIAN_POINT ( 'NONE',  ( 0.2770853660078497760, 140.6978508428007615, 501.1291105955846206 ) ) ;
#15546=CARTESIAN_POINT ( 'NONE',  ( -79.99999999999995737, 146.8256012863087108, 507.0490161104376057 ) ) ;
#15552=DIRECTION ( 'NONE',  ( -1.000000000000000000, -0.000000000000000000, -3.328238341717372086E-14 ) ) ;
#15558=VECTOR ( 'NONE', #13274, 1000.000000000000000 ) ;
#15567=ORIENTED_EDGE ( 'NONE', *, *, #446, .F. ) ;
#15568=CARTESIAN_POINT ( 'NONE',  ( -38.50085094405407204, 209.4098724938429541, 505.3921618609452935 ) ) ;
#15585=DIRECTION ( 'NONE',  ( 0.000000000000000000, -1.000000000000000000, 0.000000000000000000 ) ) ;
#15594=DIRECTION ( 'NONE',  ( 0.000000000000000000, 1.000000000000000000, 0.000000000000000000 ) ) ;
#15595=EDGE_CURVE ( 'NONE', #8340, #368, #12315, .T. ) ;
#15597=( LENGTH_UNIT ( ) NAMED_UNIT ( * ) SI_UNIT ( .MILLI., .METRE. ) );
#15603=AXIS2_PLACEMENT_3D ( 'NONE', #18753, #8049, #3204 ) ;
#15606=PLANE ( 'NONE',  #17168 ) ;
#15611=ORIENTED_EDGE ( 'NONE', *, *, #6146, .T. ) ;
#15614=EDGE_CURVE ( 'NONE', #5765, #17495, #16292, .T. ) ;
#15617=CARTESIAN_POINT ( 'NONE',  ( -0.06893388336922114112, 140.7261352223151505, 502.2905978699745333 ) ) ;
#15629=AXIS2_PLACEMENT_3D ( 'NONE', #510, #13409, #11850 ) ;
#15632=ORIENTED_EDGE ( 'NONE', *, *, #11818, .F. ) ;
#15637=VECTOR ( 'NONE', #215, 1000.000000000000000 ) ;
#15640=CARTESIAN_POINT ( 'NONE',  ( 0.000000000000000000, 316.7545334744432353, 495.1946179577816451 ) ) ;
#15646=DIRECTION ( 'NONE',  ( -1.000000000000000000, 0.000000000000000000, -0.000000000000000000 ) ) ;
#15663=VERTEX_POINT ( 'NONE', #10330 ) ;
#15664=DIRECTION ( 'NONE',  ( 0.000000000000000000, 0.000000000000000000, 1.000000000000000000 ) ) ;
#15691=SURFACE_SIDE_STYLE ('',( #10929 ) ) ;
#15694=ORIENTED_EDGE ( 'NONE', *, *, #876, .T. ) ;
#15700=CARTESIAN_POINT ( 'NONE',  ( -118.0000000000000284, 216.7545334744432921, 205.1946179577815883 ) ) ;
#15705=AXIS2_PLACEMENT_3D ( 'NONE', #13595, #1188, #4525 ) ;
#15706=CARTESIAN_POINT ( 'NONE',  ( -0.3492608071101708234, 139.7605458594808567, 500.8004217433215217 ) ) ;
#15707=EDGE_CURVE ( 'NONE', #11471, #11867, #10739, .T. ) ;
#15708=ORIENTED_EDGE ( 'NONE', *, *, #3355, .F. ) ;
#15712=ORIENTED_EDGE ( 'NONE', *, *, #1852, .T. ) ;
#15716=EDGE_CURVE ( 'NONE', #5827, #6868, #5075, .T. ) ;
#15731=SURFACE_SIDE_STYLE ('',( #12736 ) ) ;
#15740=AXIS2_PLACEMENT_3D ( 'NONE', #18874, #9413, #12503 ) ;
#15746=CARTESIAN_POINT ( 'NONE',  ( -81.18192946989263703, 147.7545334744432921, 496.6642397995874489 ) ) ;
#15747=DIRECTION ( 'NONE',  ( 0.000000000000000000, 0.000000000000000000, -1.000000000000000000 ) ) ;
#15749=DIRECTION ( 'NONE',  ( -0.000000000000000000, 1.000000000000000000, -0.000000000000000000 ) ) ;
#15750=VERTEX_POINT ( 'NONE', #7947 ) ;
#15757=VERTEX_POINT ( 'NONE', #12589 ) ;
#15758=AXIS2_PLACEMENT_3D ( 'NONE', #10475, #2637, #2938 ) ;
#15759=EDGE_CURVE ( 'NONE', #11717, #2815, #17636, .T. ) ;
#15762=CARTESIAN_POINT ( 'NONE',  ( -80.07925520782436024, 141.0520093089742204, 501.4288824830859426 ) ) ;
#15765=DIRECTION ( 'NONE',  ( 0.000000000000000000, 0.000000000000000000, -1.000000000000000000 ) ) ;
#15768=LINE ( 'NONE', #7915, #16863 ) ;
#15771=CARTESIAN_POINT ( 'NONE',  ( -38.50085094405407204, 193.0431417881923153, 505.3921618609452935 ) ) ;
#15773=LINE ( 'NONE', #10917, #3061 ) ;
#15774=CARTESIAN_POINT ( 'NONE',  ( -38.50085094405407204, 159.0821755739672483, 505.3921618609452935 ) ) ;
#15777=ORIENTED_EDGE ( 'NONE', *, *, #19712, .T. ) ;
#15792=CARTESIAN_POINT ( 'NONE',  ( -21.85283368562565443, 319.7545334744432353, 485.1700099148404774 ) ) ;
#15796=DIRECTION ( 'NONE',  ( -1.000000000000000000, -0.000000000000000000, -0.000000000000000000 ) ) ;
#15797=EDGE_CURVE ( 'NONE', #6152, #11717, #18222, .T. ) ;
#15809=EDGE_CURVE ( 'NONE', #4266, #1021, #11235, .T. ) ;
#15810=CARTESIAN_POINT ( 'NONE',  ( -0.01348608808930003983, 140.1729642737128927, 501.5297937275371964 ) ) ;
#15811=EDGE_CURVE ( 'NONE', #20015, #645, #11344, .T. ) ;
#15812=CYLINDRICAL_SURFACE ( 'NONE', #15740, 3.000000000000002665 ) ;
#15818=EDGE_CURVE ( 'NONE', #8090, #5003, #12490, .T. ) ;
#15822=EDGE_CURVE ( 'NONE', #18716, #5319, #7085, .T. ) ;
#15830=ORIENTED_EDGE ( 'NONE', *, *, #5012, .F. ) ;
#15845=DIRECTION ( 'NONE',  ( 0.000000000000000000, 0.000000000000000000, -1.000000000000000000 ) ) ;
#15848=LINE ( 'NONE', #6671, #4881 ) ;
#15854=CARTESIAN_POINT ( 'NONE',  ( -0.06173851122038213207, 138.7995772466921949, 490.1653550096017966 ) ) ;
#15860=CARTESIAN_POINT ( 'NONE',  ( -79.99999999999995737, 140.8764026050587290, 502.4686618848273270 ) ) ;
#15866=LINE ( 'NONE', #12666, #18750 ) ;
#15867=CIRCLE ( 'NONE', #13871, 1.000000000000000888 ) ;
#15870=DIRECTION ( 'NONE',  ( -0.000000000000000000, -0.000000000000000000, 1.000000000000000000 ) ) ;
#15885=ORIENTED_EDGE ( 'NONE', *, *, #12184, .T. ) ;
#15894=STYLED_ITEM ( 'NONE', ( #18401 ), #13523 ) ;
#15897=EDGE_CURVE ( 'NONE', #1482, #1591, #3109, .T. ) ;
#15902=AXIS2_PLACEMENT_3D ( 'NONE', #15746, #15951, #1573 ) ;
#15917=CARTESIAN_POINT ( 'NONE',  ( 0.7125494648445551693, 139.4936479042385997, 500.2362377901696959 ) ) ;
#15919=CARTESIAN_POINT ( 'NONE',  ( 1.181929469892510243, 139.7703989349544145, 490.5655098179848892 ) ) ;
#15921=PLANE ( 'NONE',  #8720 ) ;
#15922=ORIENTED_EDGE ( 'NONE', *, *, #978, .T. ) ;
#15938=DIRECTION ( 'NONE',  ( 0.000000000000000000, -2.775557561562888827E-14, -1.000000000000000000 ) ) ;
#15951=DIRECTION ( 'NONE',  ( 1.000000000000000000, 0.000000000000000000, 3.328238341717372086E-14 ) ) ;
#15960=( NAMED_UNIT ( * ) PLANE_ANGLE_UNIT ( ) SI_UNIT ( $, .RADIAN. ) );
#15965=CARTESIAN_POINT ( 'NONE',  ( -0.8244006410038320354, 138.9529133135991401, 489.1850737022905378 ) ) ;
#15979=CARTESIAN_POINT ( 'NONE',  ( -80.51897068092245036, 140.5128581817066902, 500.9441570819607250 ) ) ;
#15985=VERTEX_POINT ( 'NONE', #2041 ) ;
#15990=DIRECTION ( 'NONE',  ( 0.000000000000000000, 1.000000000000000000, 0.000000000000000000 ) ) ;
#16009=EDGE_CURVE ( 'NONE', #11820, #19489, #4434, .T. ) ;
#16012=AXIS2_PLACEMENT_3D ( 'NONE', #11463, #8278, #3639 ) ;
#16031=LINE ( 'NONE', #18868, #1472 ) ;
#16036=DIRECTION ( 'NONE',  ( -1.135258727068398879E-15, 3.469446951953611033E-15, 1.000000000000000000 ) ) ;
#16037=CARTESIAN_POINT ( 'NONE',  ( 1.181929469892510243, 138.7545334744432637, 490.5655098179833544 ) ) ;
#16038=FACE_OUTER_BOUND ( 'NONE', #8560, .T. ) ;
#16041=CARTESIAN_POINT ( 'NONE',  ( -78.99999999999995737, 140.1563709946295262, 488.5655098179835818 ) ) ;
#16048=EDGE_CURVE ( 'NONE', #13854, #7676, #3458, .T. ) ;
#16067=( BOUNDED_SURFACE ( )  B_SPLINE_SURFACE ( 3, 2, ( 
 ( #14140, #14246, #230 ),
 ( #12603, #6225, #1550 ),
 ( #7774, #7861, #15917 ),
 ( #26, #3010, #14054 ),
 ( #4783, #123, #18873 ),
 ( #9505, #1456, #1761 ),
 ( #11065, #17343, #8076 ),
 ( #4983, #3226, #11253 ),
 ( #6436, #18773, #9304 ),
 ( #12502, #17535, #14452 ),
 ( #4569, #15810, #1648 ),
 ( #4878, #10851, #7962 ),
 ( #3437, #12723, #6133 ),
 ( #6531, #18975, #11154 ),
 ( #17432, #15617, #3324 ),
 ( #12819, #19075, #1864 ) ),
 .UNSPECIFIED., .F., .F., .T. ) 
 B_SPLINE_SURFACE_WITH_KNOTS ( ( 4, 2, 2, 2, 2, 2, 2, 4 ),
 ( 3, 3 ),
 ( 0.001246970379171045062, 0.001676325320858793304, 0.002105680262546541764, 0.002535035204234289789, 0.002964390145922038249, 0.003393745087609786708, 0.003823100029297534733, 0.004681809912673031218 ),
 ( 0.000000000000000000, 1.000000000000000000 ),
 .UNSPECIFIED. ) 
 GEOMETRIC_REPRESENTATION_ITEM ( )  RATIONAL_B_SPLINE_SURFACE ( (
 ( 1.000000000000000000, 0.8351454326190185240, 1.000000000000000000),
 ( 1.000000000000000000, 0.8351391024961110077, 1.000000000000000000),
 ( 1.000000000000000000, 0.8348195684913958248, 1.000000000000000000),
 ( 1.000000000000000000, 0.8333905549599697204, 1.000000000000000000),
 ( 1.000000000000000000, 0.8322627347962558986, 1.000000000000000000),
 ( 1.000000000000000000, 0.8289108061541168304, 1.000000000000000000),
 ( 1.000000000000000000, 0.8266665721634388619, 1.000000000000000000),
 ( 1.000000000000000000, 0.8205566980956985335, 1.000000000000000000),
 ( 1.000000000000000000, 0.8167651399558516490, 1.000000000000000000),
 ( 1.000000000000000000, 0.8072326331355020868, 1.000000000000000000),
 ( 1.000000000000000000, 0.8014496535022105350, 1.000000000000000000),
 ( 1.000000000000000000, 0.7879847800020959303, 1.000000000000000000),
 ( 1.000000000000000000, 0.7802402271099223574, 1.000000000000000000),
 ( 1.000000000000000000, 0.7537145741180295566, 1.000000000000000000),
 ( 1.000000000000000000, 0.7323456299789787849, 1.000000000000000000),
 ( 1.000000000000000000, 0.7071067811865475727, 1.000000000000000000) ) ) 
 REPRESENTATION_ITEM ( '' )  SURFACE ( )  );
#16096=ORIENTED_EDGE ( 'NONE', *, *, #4771, .F. ) ;
#16109=DIRECTION ( 'NONE',  ( -0.000000000000000000, -0.000000000000000000, 1.000000000000000000 ) ) ;
#16123=VERTEX_POINT ( 'NONE', #15568 ) ;
#16127=ORIENTED_EDGE ( 'NONE', *, *, #3023, .F. ) ;
#16134=PLANE ( 'NONE',  #4429 ) ;
#16153=CARTESIAN_POINT ( 'NONE',  ( 2.181929469892510465, 216.7545334744432921, 490.5655098179832976 ) ) ;
#16177=CARTESIAN_POINT ( 'NONE',  ( -80.20845338047620032, 140.7853878564479828, 501.2089312876914846 ) ) ;
#16179=DIRECTION ( 'NONE',  ( -1.000000000000000000, 0.000000000000000000, 7.715811803773179210E-14 ) ) ;
#16185=DIRECTION ( 'NONE',  ( -0.000000000000000000, -1.000000000000000000, -0.000000000000000000 ) ) ;
#16199=CARTESIAN_POINT ( 'NONE',  ( -81.18192946989111647, 138.7545334744432637, 489.5655098179833544 ) ) ;
#16207=LINE ( 'NONE', #16311, #4055 ) ;
#16214=LINE ( 'NONE', #11551, #4102 ) ;
#16224=AXIS2_PLACEMENT_3D ( 'NONE', #4675, #3337, #20331 ) ;
#16233=DIRECTION ( 'NONE',  ( -3.328238341717372086E-14, 0.000000000000000000, 1.000000000000000000 ) ) ;
#16237=EDGE_LOOP ( 'NONE', ( #10316, #15061, #3889, #18948, #5328, #3544, #3842, #15126, #347, #761 ) ) ;
#16242=ORIENTED_EDGE ( 'NONE', *, *, #2322, .T. ) ;
#16253=CARTESIAN_POINT ( 'NONE',  ( 1.000000000001310063, 139.7703989349544145, 489.5655098179835818 ) ) ;
#16257=VECTOR ( 'NONE', #4866, 1000.000000000000000 ) ;
#16258=( LENGTH_UNIT ( ) NAMED_UNIT ( * ) SI_UNIT ( .MILLI., .METRE. ) );
#16259=LINE ( 'NONE', #3769, #3147 ) ;
#16262=EDGE_LOOP ( 'NONE', ( #10593, #3001 ) ) ;
#16268=CARTESIAN_POINT ( 'NONE',  ( -1.336826079150933300E-12, 139.7703989349544145, 489.5655098179848892 ) ) ;
#16271=VECTOR ( 'NONE', #10780, 1000.000000000000000 ) ;
#16285=CARTESIAN_POINT ( 'NONE',  ( 0.3790268517283566507, 139.8046609698958775, 489.3602998400258457 ) ) ;
#16287=DIRECTION ( 'NONE',  ( 1.000000000000000000, 0.000000000000000000, 0.000000000000000000 ) ) ;
#16292=CIRCLE ( 'NONE', #6407, 1.000000000000000888 ) ;
#16296=EDGE_LOOP ( 'NONE', ( #9318, #7914, #18569, #7985 ) ) ;
#16304=STYLED_ITEM ( 'NONE', ( #52 ), #12428 ) ;
#16311=CARTESIAN_POINT ( 'NONE',  ( -44.50085094405409336, 193.0431417881923153, 505.3921618609452935 ) ) ;
#16314=CIRCLE ( 'NONE', #10040, 1.000000000000000888 ) ;
#16320=AXIS2_PLACEMENT_3D ( 'NONE', #12726, #11469, #17752 ) ;
#16321=LINE ( 'NONE', #3725, #9034 ) ;
#16331=VERTEX_POINT ( 'NONE', #4110 ) ;
#16334=FACE_OUTER_BOUND ( 'NONE', #2532, .T. ) ;
#16335=CARTESIAN_POINT ( 'NONE',  ( -78.99999999999995737, 146.8256012863087108, 507.0490161104376057 ) ) ;
#16346=LINE ( 'NONE', #12933, #4253 ) ;
#16348=CIRCLE ( 'NONE', #14334, 3.000000000000002665 ) ;
#16350=EDGE_CURVE ( 'NONE', #4262, #9522, #9204, .T. ) ;
#16368=DIRECTION ( 'NONE',  ( 0.000000000000000000, 1.000000000000000000, 1.632680918566406793E-16 ) ) ;
#16372=CARTESIAN_POINT ( 'NONE',  ( 0.9999999999999872324, 216.7545334744432921, 488.5655098179835818 ) ) ;
#16382=CARTESIAN_POINT ( 'NONE',  ( -1.000000000000011768, 142.0976792249508946, 502.3210940490797611 ) ) ;
#16387=CARTESIAN_POINT ( 'NONE',  ( -1.000000000000013101, 139.2066006846527841, 488.2525619656395861 ) ) ;
#16388=LINE ( 'NONE', #5244, #5400 ) ;
#16405=DIRECTION ( 'NONE',  ( 0.000000000000000000, 1.000000000000000000, -0.000000000000000000 ) ) ;
#16406=AXIS2_PLACEMENT_3D ( 'NONE', #15401, #1231, #20226 ) ;
#16407=SURFACE_STYLE_USAGE ( .BOTH. , #5365 ) ;
#16414=DIRECTION ( 'NONE',  ( 0.000000000000000000, 0.000000000000000000, -1.000000000000000000 ) ) ;
#16425=LINE ( 'NONE', #5577, #18240 ) ;
#16436=EDGE_LOOP ( 'NONE', ( #9653, #14885, #18012, #10442 ) ) ;
#16451=CARTESIAN_POINT ( 'NONE',  ( -1.000000000000001110, 138.7545334744432637, 478.3411705753777596 ) ) ;
#16453=CARTESIAN_POINT ( 'NONE',  ( -64.99999999999995737, 317.7545334744432353, 495.1946179577816451 ) ) ;
#16454=FACE_OUTER_BOUND ( 'NONE', #5433, .T. ) ;
#16460=ORIENTED_EDGE ( 'NONE', *, *, #16964, .F. ) ;
#16463=EDGE_LOOP ( 'NONE', ( #11573, #763, #12230, #113 ) ) ;
#16472=( NAMED_UNIT ( * ) PLANE_ANGLE_UNIT ( ) SI_UNIT ( $, .RADIAN. ) );
#16475=EDGE_CURVE ( 'NONE', #15985, #7546, #361, .T. ) ;
#16476=CARTESIAN_POINT ( 'NONE',  ( -0.8056780331109345550, 138.9431362660446609, 489.2309999112469541 ) ) ;
#16478=DIRECTION ( 'NONE',  ( -1.000000000000000000, 0.000000000000000000, 0.000000000000000000 ) ) ;
#16489=EDGE_LOOP ( 'NONE', ( #14058, #6798, #13559, #4639 ) ) ;
#16490=( NAMED_UNIT ( * ) PLANE_ANGLE_UNIT ( ) SI_UNIT ( $, .RADIAN. ) );
#16496=CARTESIAN_POINT ( 'NONE',  ( -80.99999999999995737, 138.7545334744432637, 488.5655098179835818 ) ) ;
#16502=DIRECTION ( 'NONE',  ( 0.000000000000000000, 0.000000000000000000, -1.000000000000000000 ) ) ;
#16504=CARTESIAN_POINT ( 'NONE',  ( 2.181929469892549545, 139.7545334744432637, 491.0690926367355473 ) ) ;
#16508=ORIENTED_EDGE ( 'NONE', *, *, #2145, .T. ) ;
#16509=VECTOR ( 'NONE', #9533, 1000.000000000000000 ) ;
#16522=DIRECTION ( 'NONE',  ( 1.000000000000000000, 0.000000000000000000, 1.322948291343119651E-12 ) ) ;
#16533=EDGE_CURVE ( 'NONE', #2216, #5003, #5919, .T. ) ;
#16539=DIRECTION ( 'NONE',  ( -5.551115123125782071E-14, 1.203706215242021147E-29, -1.000000000000000000 ) ) ;
#16540=UNCERTAINTY_MEASURE_WITH_UNIT (LENGTH_MEASURE( 1.000000000000000082E-05 ), #19040, 'distance_accuracy_value', 'NONE');
#16543=CARTESIAN_POINT ( 'NONE',  ( -80.25208250843274982, 139.5548694108364316, 500.3753056083104411 ) ) ;
#16545=DIRECTION ( 'NONE',  ( -0.000000000000000000, 1.000000000000000000, -0.000000000000000000 ) ) ;
#16551=CARTESIAN_POINT ( 'NONE',  ( 0.000000000000000000, 316.7545334744432921, 155.1946179577816167 ) ) ;
#16562=( GEOMETRIC_REPRESENTATION_CONTEXT ( 3 ) GLOBAL_UNCERTAINTY_ASSIGNED_CONTEXT ( ( #13063 ) ) GLOBAL_UNIT_ASSIGNED_CONTEXT ( ( #16258, #16734, #6666 ) ) REPRESENTATION_CONTEXT ( 'NONE', 'WORKASPACE' ) );
#16563=VECTOR ( 'NONE', #16233, 1000.000000000000000 ) ;
#16570=DIRECTION ( 'NONE',  ( 3.328238341717372086E-14, 0.000000000000000000, -1.000000000000000000 ) ) ;
#16575=DIRECTION ( 'NONE',  ( -1.000000000000000000, -0.000000000000000000, -0.000000000000000000 ) ) ;
#16581=AXIS2_PLACEMENT_3D ( 'NONE', #4840, #18937, #4730 ) ;
#16583=DIRECTION ( 'NONE',  ( 0.000000000000000000, -0.000000000000000000, -1.000000000000000000 ) ) ;
#16585=DIRECTION ( 'NONE',  ( -0.000000000000000000, 0.000000000000000000, 1.000000000000000000 ) ) ;
#16586=DIRECTION ( 'NONE',  ( 1.000000000000000000, 0.000000000000000000, -0.000000000000000000 ) ) ;
#16609=( NAMED_UNIT ( * ) PLANE_ANGLE_UNIT ( ) SI_UNIT ( $, .RADIAN. ) );
#16622=VERTEX_POINT ( 'NONE', #8027 ) ;
#16635=CARTESIAN_POINT ( 'NONE',  ( -79.99999999999995737, 216.7545334744432921, 495.1946179577816451 ) ) ;
#16638=VECTOR ( 'NONE', #10243, 1000.000000000000000 ) ;
#16645=ORIENTED_EDGE ( 'NONE', *, *, #15420, .T. ) ;
#16659=CARTESIAN_POINT ( 'NONE',  ( -78.99999999999995737, 140.8764026050586722, 502.4686618848272133 ) ) ;
#16666=PLANE ( 'NONE',  #4893 ) ;
#16674=AXIS2_PLACEMENT_3D ( 'NONE', #6957, #5112, #13060 ) ;
#16682=( LENGTH_UNIT ( ) NAMED_UNIT ( * ) SI_UNIT ( .MILLI., .METRE. ) );
#16686=CARTESIAN_POINT ( 'NONE',  ( -0.9999999956396431466, 139.1133280296707824, 488.5356365985891216 ) ) ;
#16687=CYLINDRICAL_SURFACE ( 'NONE', #468, 3.883636366625808911 ) ;
#16688=CYLINDRICAL_SURFACE ( 'NONE', #8171, 1.000000000000000888 ) ;
#16705=FACE_OUTER_BOUND ( 'NONE', #14791, .T. ) ;
#16721=SHAPE_REPRESENTATION ( 'Part12^Assem2', ( #2741 ), #14604 ) ;
#16722=ORIENTED_EDGE ( 'NONE', *, *, #7689, .T. ) ;
#16723=ORIENTED_EDGE ( 'NONE', *, *, #11529, .F. ) ;
#16724=EDGE_CURVE ( 'NONE', #17622, #2022, #652, .T. ) ;
#16734=( NAMED_UNIT ( * ) PLANE_ANGLE_UNIT ( ) SI_UNIT ( $, .RADIAN. ) );
#16737=DIRECTION ( 'NONE',  ( 1.000000000000000000, 0.000000000000000000, 0.000000000000000000 ) ) ;
#16741=DIRECTION ( 'NONE',  ( 0.000000000000000000, -1.000000000000000000, 0.000000000000000000 ) ) ;
#16755=CIRCLE ( 'NONE', #592, 1.000000000000000888 ) ;
#16765=ORIENTED_EDGE ( 'NONE', *, *, #13292, .T. ) ;
#16776=ADVANCED_FACE ( 'NONE', ( #16454 ), #19916, .T. ) ;
#16786=AXIS2_PLACEMENT_3D ( 'NONE', #10673, #20024, #12324 ) ;
#16792=CARTESIAN_POINT ( 'NONE',  ( -15.00000000000000000, 316.7545334744432353, 495.1946179577816451 ) ) ;
#16798=PRESENTATION_STYLE_ASSIGNMENT (( #1190 ) ) ;
#16800=CYLINDRICAL_SURFACE ( 'NONE', #2066, 3.000000000000002665 ) ;
#16802=CIRCLE ( 'NONE', #16786, 3.000000000000002665 ) ;
#16803=EDGE_CURVE ( 'NONE', #3885, #19179, #10247, .T. ) ;
#16806=DIRECTION ( 'NONE',  ( 5.551115123125777022E-14, 0.000000000000000000, -1.000000000000000000 ) ) ;
#16807=EDGE_CURVE ( 'NONE', #3908, #1145, #8596, .T. ) ;
#16809=ORIENTED_EDGE ( 'NONE', *, *, #18808, .F. ) ;
#16810=VERTEX_POINT ( 'NONE', #2409 ) ;
#16818=VECTOR ( 'NONE', #11984, 1000.000000000000000 ) ;
#16821=EDGE_CURVE ( 'NONE', #13927, #14143, #15099, .T. ) ;
#16827=DIRECTION ( 'NONE',  ( 0.000000000000000000, 0.000000000000000000, -1.000000000000000000 ) ) ;
#16829=CARTESIAN_POINT ( 'NONE',  ( -80.49355071749218382, 139.7917123817078959, 489.4303101983043689 ) ) ;
#16832=ORIENTED_EDGE ( 'NONE', *, *, #2858, .F. ) ;
#16846=CARTESIAN_POINT ( 'NONE',  ( -80.01145065471625628, 141.3451996134640751, 501.6408122255736544 ) ) ;
#16854=ORIENTED_EDGE ( 'NONE', *, *, #8169, .T. ) ;
#16861=ADVANCED_FACE ( 'NONE', ( #13847 ), #9310, .T. ) ;
#16863=VECTOR ( 'NONE', #12981, 1000.000000000000000 ) ;
#16866=CARTESIAN_POINT ( 'NONE',  ( 0.6600482361318578128, 140.4535475171542771, 500.8793675648332169 ) ) ;
#16872=MECHANICAL_DESIGN_GEOMETRIC_PRESENTATION_REPRESENTATION('',(#9279),#12253);
#16878=SURFACE_STYLE_FILL_AREA ( #8836 ) ;
#16889=STYLED_ITEM ( 'NONE', ( #9486 ), #18329 ) ;
#16920=DIRECTION ( 'NONE',  ( 1.000000000000000000, -0.000000000000000000, -0.000000000000000000 ) ) ;
#16923=MECHANICAL_DESIGN_GEOMETRIC_PRESENTATION_REPRESENTATION('',(#9643),#3416);
#16925=CARTESIAN_POINT ( 'NONE',  ( -41.50085094405408626, 193.0431417881923153, 510.3921618609452935 ) ) ;
#16926=DIRECTION ( 'NONE',  ( -0.000000000000000000, 0.000000000000000000, 1.000000000000000000 ) ) ;
#16929=ORIENTED_EDGE ( 'NONE', *, *, #11025, .T. ) ;
#16934=EDGE_CURVE ( 'NONE', #9586, #6469, #20119, .T. ) ;
#16937=ORIENTED_EDGE ( 'NONE', *, *, #5552, .T. ) ;
#16947=DIRECTION ( 'NONE',  ( 1.000000000000000000, 0.000000000000000000, 0.000000000000000000 ) ) ;
#16949=EDGE_CURVE ( 'NONE', #17127, #11075, #985, .T. ) ;
#16957=CARTESIAN_POINT ( 'NONE',  ( 0.000000000000000000, 0.000000000000000000, 515.1946179577817020 ) ) ;
#16964=EDGE_CURVE ( 'NONE', #16331, #4741, #13838, .T. ) ;
#16966=AXIS2_PLACEMENT_3D ( 'NONE', #1032, #13647, #13944 ) ;
#16969=VERTEX_POINT ( 'NONE', #14458 ) ;
#16970=CIRCLE ( 'NONE', #15340, 1.000000000000000888 ) ;
#16981=( NAMED_UNIT ( * ) PLANE_ANGLE_UNIT ( ) SI_UNIT ( $, .RADIAN. ) );
#16982=DIRECTION ( 'NONE',  ( 1.000000000000000000, -0.000000000000000000, -0.000000000000000000 ) ) ;
#16988=PLANE ( 'NONE',  #9291 ) ;
#16992=ORIENTED_EDGE ( 'NONE', *, *, #18547, .F. ) ;
#17013=ORIENTED_EDGE ( 'NONE', *, *, #446, .T. ) ;
#17017=CARTESIAN_POINT ( 'NONE',  ( 0.000000000000000000, 317.7545334744432353, 1.632680918566406547E-16 ) ) ;
#17023=CYLINDRICAL_SURFACE ( 'NONE', #996, 3.000000000000002665 ) ;
#17029=( NAMED_UNIT ( * ) SI_UNIT ( $, .STERADIAN. ) SOLID_ANGLE_UNIT ( ) );
#17032=DIRECTION ( 'NONE',  ( -0.000000000000000000, 1.000000000000000000, -0.000000000000000000 ) ) ;
#17041=CARTESIAN_POINT ( 'NONE',  ( -41.50085094405408626, 209.4098724938429541, 510.3921618609452935 ) ) ;
#17050=CARTESIAN_POINT ( 'NONE',  ( 0.000000000000000000, 316.7545334744432353, 515.1946179577817020 ) ) ;
#17056=EDGE_LOOP ( 'NONE', ( #17200, #18155, #19200, #1974 ) ) ;
#17061=CARTESIAN_POINT ( 'NONE',  ( -38.50085094405407204, 209.4098724938429541, 510.3921618609452935 ) ) ;
#17064=CARTESIAN_POINT ( 'NONE',  ( -79.99999999999995737, 219.7545334744433205, 515.1946179577817020 ) ) ;
#17066=CARTESIAN_POINT ( 'NONE',  ( -79.99999999999995737, 142.0976792249508946, 502.3210940490797611 ) ) ;
#17071=LINE ( 'NONE', #9031, #18681 ) ;
#17075=EDGE_CURVE ( 'NONE', #17453, #4266, #17659, .T. ) ;
#17088=CARTESIAN_POINT ( 'NONE',  ( -44.50085094405407915, 175.4489062796178871, 505.3921618609452935 ) ) ;
#17104=CARTESIAN_POINT ( 'NONE',  ( 1.000000000001310063, 139.7703989349544145, 489.5655098179835818 ) ) ;
#17127=VERTEX_POINT ( 'NONE', #20068 ) ;
#17131=VECTOR ( 'NONE', #10455, 1000.000000000000000 ) ;
#17138=DIRECTION ( 'NONE',  ( 1.000000000000000000, 0.000000000000000000, -1.322948291343117631E-12 ) ) ;
#17144=EDGE_CURVE ( 'NONE', #16810, #17234, #9236, .T. ) ;
#17145=ORIENTED_EDGE ( 'NONE', *, *, #890, .F. ) ;
#17153=VERTEX_POINT ( 'NONE', #4140 ) ;
#17164=CARTESIAN_POINT ( 'NONE',  ( -1.000000000000014655, 152.4824555358011082, 486.3411705753778165 ) ) ;
#17167=CARTESIAN_POINT ( 'NONE',  ( -1.000000000000012657, 139.1177163613726577, 488.5223183823763407 ) ) ;
#17168=AXIS2_PLACEMENT_3D ( 'NONE', #2530, #2315, #15109 ) ;
#17172=ADVANCED_FACE ( 'NONE', ( #13896 ), #15527, .T. ) ;
#17176=STYLED_ITEM ( 'NONE', ( #18595 ), #17818 ) ;
#17179=EDGE_CURVE ( 'NONE', #16123, #9243, #12369, .T. ) ;
#17200=ORIENTED_EDGE ( 'NONE', *, *, #473, .T. ) ;
#17202=ORIENTED_EDGE ( 'NONE', *, *, #12912, .F. ) ;
#17204=SURFACE_STYLE_USAGE ( .BOTH. , #15691 ) ;
#17209=DIRECTION ( 'NONE',  ( 1.450371633464474201E-15, 0.000000000000000000, 1.000000000000000000 ) ) ;
#17213=( LENGTH_UNIT ( ) NAMED_UNIT ( * ) SI_UNIT ( .MILLI., .METRE. ) );
#17219=CLOSED_SHELL ( 'NONE', ( #17818, #19095, #2851, #3975, #170, #13523 ) ) ;
#17220=VERTEX_POINT ( 'NONE', #11213 ) ;
#17234=VERTEX_POINT ( 'NONE', #12466 ) ;
#17237=SURFACE_STYLE_USAGE ( .BOTH. , #14052 ) ;
#17250=EDGE_CURVE ( 'NONE', #16622, #10073, #3323, .T. ) ;
#17259=LINE ( 'NONE', #9615, #9730 ) ;
#17269=CARTESIAN_POINT ( 'NONE',  ( -80.17878486073050226, 139.8636771835041372, 489.1515118754280138 ) ) ;
#17288=CARTESIAN_POINT ( 'NONE',  ( -80.03794136217337041, 139.6076487680217042, 500.4896316014566651 ) ) ;
#17293=ADVANCED_FACE ( 'NONE', ( #1606 ), #10910, .T. ) ;
#17305=PLANE ( 'NONE',  #4739 ) ;
#17310=EDGE_CURVE ( 'NONE', #19125, #17405, #5326, .T. ) ;
#17318=CARTESIAN_POINT ( 'NONE',  ( -58.16843972078500258, 319.7545334744432353, 485.1700099148404206 ) ) ;
#17343=CARTESIAN_POINT ( 'NONE',  ( 0.3141013587250581218, 139.8869819025744334, 501.0706778502146790 ) ) ;
#17352=SPHERICAL_SURFACE ( 'NONE', #16224, 1.000000000000000000 ) ;
#17367=FACE_OUTER_BOUND ( 'NONE', #17056, .T. ) ;
#17369=DIRECTION ( 'NONE',  ( 0.000000000000000000, -1.000000000000000000, 0.000000000000000000 ) ) ;
#17370=SURFACE_STYLE_USAGE ( .BOTH. , #13980 ) ;
#17372=PLANE ( 'NONE',  #8632 ) ;
#17374=CARTESIAN_POINT ( 'NONE',  ( 1.181929469892505358, 138.7723821175183048, 490.5025619656410640 ) ) ;
#17375=( LENGTH_UNIT ( ) NAMED_UNIT ( * ) SI_UNIT ( .MILLI., .METRE. ) );
#17380=VERTEX_POINT ( 'NONE', #17908 ) ;
#17382=ORIENTED_EDGE ( 'NONE', *, *, #15797, .F. ) ;
#17384=CARTESIAN_POINT ( 'NONE',  ( -80.71241711305556521, 140.4313724365906353, 500.8555218219611334 ) ) ;
#17405=VERTEX_POINT ( 'NONE', #1917 ) ;
#17413=AXIS2_PLACEMENT_3D ( 'NONE', #18728, #6076, #18819 ) ;
#17421=EDGE_CURVE ( 'NONE', #2723, #645, #8237, .T. ) ;
#17430=CARTESIAN_POINT ( 'NONE',  ( 0.000000000000000000, 219.7545334744432921, 515.1946179577817020 ) ) ;
#17432=CARTESIAN_POINT ( 'NONE',  ( -1.214306433183764966E-14, 141.4538060686001302, 501.7130291278048162 ) ) ;
#17434=DIRECTION ( 'NONE',  ( -1.000000000000000000, -0.000000000000000000, -0.000000000000000000 ) ) ;
#17436=CARTESIAN_POINT ( 'NONE',  ( -1.387778780781445676E-14, 138.7545334744432637, 489.5655098179848892 ) ) ;
#17442=VECTOR ( 'NONE', #10489, 1000.000000000000000 ) ;
#17450=ORIENTED_EDGE ( 'NONE', *, *, #12446, .F. ) ;
#17452=AXIS2_PLACEMENT_3D ( 'NONE', #5563, #6441, #19300 ) ;
#17453=VERTEX_POINT ( 'NONE', #1071 ) ;
#17458=DIRECTION ( 'NONE',  ( 0.000000000000000000, 0.000000000000000000, -1.000000000000000000 ) ) ;
#17466=DIRECTION ( 'NONE',  ( -1.000000000000000000, 8.315472005415352149E-14, -1.318389841601051321E-12 ) ) ;
#17469=EDGE_CURVE ( 'NONE', #10840, #18058, #4301, .T. ) ;
#17471=ORIENTED_EDGE ( 'NONE', *, *, #19660, .F. ) ;
#17472=AXIS2_PLACEMENT_3D ( 'NONE', #11318, #3284, #18735 ) ;
#17476=ORIENTED_EDGE ( 'NONE', *, *, #1682, .F. ) ;
#17478=CARTESIAN_POINT ( 'NONE',  ( -79.93116660809441498, 140.2969627923933729, 501.7130883271435096 ) ) ;
#17491=ORIENTED_EDGE ( 'NONE', *, *, #2283, .T. ) ;
#17495=VERTEX_POINT ( 'NONE', #1176 ) ;
#17506=CIRCLE ( 'NONE', #5030, 0.9999999999999453770 ) ;
#17517=( GEOMETRIC_REPRESENTATION_CONTEXT ( 3 ) GLOBAL_UNCERTAINTY_ASSIGNED_CONTEXT ( ( #9941 ) ) GLOBAL_UNIT_ASSIGNED_CONTEXT ( ( #353, #11394, #15071 ) ) REPRESENTATION_CONTEXT ( 'NONE', 'WORKASPACE' ) );
#17535=CARTESIAN_POINT ( 'NONE',  ( 0.02524115952202954025, 140.1151673599038645, 501.4410921460604413 ) ) ;
#17546=PLANE ( 'NONE',  #12919 ) ;
#17553=ORIENTED_EDGE ( 'NONE', *, *, #324, .T. ) ;
#17556=ORIENTED_EDGE ( 'NONE', *, *, #8146, .T. ) ;
#17560=ORIENTED_EDGE ( 'NONE', *, *, #10033, .T. ) ;
#17561=EDGE_CURVE ( 'NONE', #19713, #13515, #15129, .T. ) ;
#17576=DIRECTION ( 'NONE',  ( -1.000000000000000000, -0.000000000000000000, -3.328238341717372086E-14 ) ) ;
#17584=EDGE_CURVE ( 'NONE', #19713, #7546, #12568, .T. ) ;
#17591=CARTESIAN_POINT ( 'NONE',  ( -80.17038797525196969, 140.8458045485498360, 501.2617728964195862 ) ) ;
#17620=CIRCLE ( 'NONE', #7733, 8.000000000000007105 ) ;
#17622=VERTEX_POINT ( 'NONE', #8601 ) ;
#17632=DIRECTION ( 'NONE',  ( 1.000000000000000000, 0.000000000000000000, 3.328238341717372086E-14 ) ) ;
#17633=APPLICATION_CONTEXT ( 'automotive_design' ) ;
#17636=LINE ( 'NONE', #14229, #4088 ) ;
#17645=DIRECTION ( 'NONE',  ( -0.000000000000000000, -1.000000000000000000, -1.632680918566406547E-16 ) ) ;
#17649=VECTOR ( 'NONE', #5870, 1000.000000000000000 ) ;
#17652=VECTOR ( 'NONE', #10588, 1000.000000000000000 ) ;
#17654=PLANE ( 'NONE',  #20150 ) ;
#17659=LINE ( 'NONE', #3546, #10224 ) ;
#17660=DIRECTION ( 'NONE',  ( 1.000000000000000000, 0.000000000000000000, 0.000000000000000000 ) ) ;
#17664=FACE_OUTER_BOUND ( 'NONE', #10720, .T. ) ;
#17672=CARTESIAN_POINT ( 'NONE',  ( 0.3607327643218288804, 139.8077789474102133, 489.3460758413267513 ) ) ;
#17687=DIRECTION ( 'NONE',  ( 1.000000000000000000, 0.000000000000000000, 0.000000000000000000 ) ) ;
#17694=CARTESIAN_POINT ( 'NONE',  ( -79.99999999999995737, 141.4538982823126503, 501.7130837607361968 ) ) ;
#17697=FILL_AREA_STYLE_COLOUR ( '', #2700 ) ;
#17698=ORIENTED_EDGE ( 'NONE', *, *, #13866, .F. ) ;
#17711=EDGE_CURVE ( 'NONE', #15663, #15103, #15867, .T. ) ;
#17721=CARTESIAN_POINT ( 'NONE',  ( -81.18192946989242387, 139.7703989349477354, 490.5655098180907885 ) ) ;
#17729=ADVANCED_FACE ( 'NONE', ( #1997 ), #19116, .F. ) ;
#17733=EDGE_CURVE ( 'NONE', #15663, #17495, #3575, .T. ) ;
#17735=DIRECTION ( 'NONE',  ( -1.000000000000000000, 0.000000000000000000, 0.000000000000000000 ) ) ;
#17740=UNCERTAINTY_MEASURE_WITH_UNIT (LENGTH_MEASURE( 1.000000000000000082E-05 ), #6357, 'distance_accuracy_value', 'NONE');
#17748=CARTESIAN_POINT ( 'NONE',  ( -78.99999999999995737, 146.8256012863087676, 480.6843163258853906 ) ) ;
#17752=DIRECTION ( 'NONE',  ( 0.000000000000000000, 0.000000000000000000, -1.000000000000000000 ) ) ;
#17774=CIRCLE ( 'NONE', #20047, 1.000000000000000000 ) ;
#17775=DIRECTION ( 'NONE',  ( 0.000000000000000000, 0.000000000000000000, 1.000000000000000000 ) ) ;
#17778=SURFACE_STYLE_FILL_AREA ( #11713 ) ;
#17797=CARTESIAN_POINT ( 'NONE',  ( -0.2419462974620343876, 138.8109269117517499, 490.0408395169303617 ) ) ;
#17807=ADVANCED_FACE ( 'NONE', ( #11913 ), #15102, .T. ) ;
#17813=SURFACE_STYLE_USAGE ( .BOTH. , #5462 ) ;
#17818=ADVANCED_FACE ( 'NONE', ( #15521 ), #6445, .F. ) ;
#17821=CARTESIAN_POINT ( 'NONE',  ( -79.99999999999995737, 216.7545334744432921, 495.1946179577816451 ) ) ;
#17833=ORIENTED_EDGE ( 'NONE', *, *, #18807, .F. ) ;
#17836=ORIENTED_EDGE ( 'NONE', *, *, #12446, .T. ) ;
#17838=AXIS2_PLACEMENT_3D ( 'NONE', #11210, #3390, #10919 ) ;
#17839=( GEOMETRIC_REPRESENTATION_CONTEXT ( 3 ) GLOBAL_UNCERTAINTY_ASSIGNED_CONTEXT ( ( #1208 ) ) GLOBAL_UNIT_ASSIGNED_CONTEXT ( ( #12422, #9423, #6144 ) ) REPRESENTATION_CONTEXT ( 'NONE', 'WORKASPACE' ) );
#17857=ADVANCED_FACE ( 'NONE', ( #10765 ), #13569, .T. ) ;
#17862=VERTEX_POINT ( 'NONE', #12304 ) ;
#17868=ORIENTED_EDGE ( 'NONE', *, *, #9764, .F. ) ;
#17871=( GEOMETRIC_REPRESENTATION_CONTEXT ( 3 ) GLOBAL_UNCERTAINTY_ASSIGNED_CONTEXT ( ( #4155 ) ) GLOBAL_UNIT_ASSIGNED_CONTEXT ( ( #15597, #7843, #17029 ) ) REPRESENTATION_CONTEXT ( 'NONE', 'WORKASPACE' ) );
#17872=DIRECTION ( 'NONE',  ( -0.000000000000000000, 1.000000000000000000, -0.000000000000000000 ) ) ;
#17873=ADVANCED_FACE ( 'NONE', ( #7674 ), #17352, .T. ) ;
#17874=DIRECTION ( 'NONE',  ( 0.000000000000000000, 1.000000000000000000, -0.000000000000000000 ) ) ;
#17889=CARTESIAN_POINT ( 'NONE',  ( -1.000000000000015765, 147.7545334744432921, 491.0690926367356042 ) ) ;
#17893=CIRCLE ( 'NONE', #6395, 1.000000000000000888 ) ;
#17894=EDGE_LOOP ( 'NONE', ( #17836, #61, #971, #12691 ) ) ;
#17897=CARTESIAN_POINT ( 'NONE',  ( -1.301042606982605321E-14, 140.1563709946295262, 488.5655098179835818 ) ) ;
#17908=CARTESIAN_POINT ( 'NONE',  ( 2.181929469893224560, 140.4048636633015406, 499.8237260975781169 ) ) ;
#17909=ORIENTED_EDGE ( 'NONE', *, *, #5741, .F. ) ;
#17913=ORIENTED_EDGE ( 'NONE', *, *, #6892, .F. ) ;
#17921=AXIS2_PLACEMENT_3D ( 'NONE', #9698, #6419, #3526 ) ;
#17924=FACE_OUTER_BOUND ( 'NONE', #1642, .T. ) ;
#17940=CIRCLE ( 'NONE', #11351, 3.883636366625808911 ) ;
#17943=ORIENTED_EDGE ( 'NONE', *, *, #2434, .T. ) ;
#17944=EDGE_CURVE ( 'NONE', #17453, #15750, #19143, .T. ) ;
#17963=DIRECTION ( 'NONE',  ( 0.000000000000000000, 1.000000000000000000, 0.000000000000000000 ) ) ;
#17978=CARTESIAN_POINT ( 'NONE',  ( -38.50085094405407204, 175.4489062796178871, 505.3921618609452935 ) ) ;
#17981=FACE_OUTER_BOUND ( 'NONE', #3116, .T. ) ;
#17996=SURFACE_STYLE_USAGE ( .BOTH. , #9966 ) ;
#18012=ORIENTED_EDGE ( 'NONE', *, *, #10412, .F. ) ;
#18015=FACE_OUTER_BOUND ( 'NONE', #18477, .T. ) ;
#18019=PRESENTATION_STYLE_ASSIGNMENT (( #16407 ) ) ;
#18028=ORIENTED_EDGE ( 'NONE', *, *, #13171, .T. ) ;
#18033=ADVANCED_FACE ( 'NONE', ( #17664 ), #17546, .F. ) ;
#18037=FACE_OUTER_BOUND ( 'NONE', #1220, .T. ) ;
#18044=AXIS2_PLACEMENT_3D ( 'NONE', #16041, #4573, #14144 ) ;
#18048=( LENGTH_UNIT ( ) NAMED_UNIT ( * ) SI_UNIT ( .MILLI., .METRE. ) );
#18050=ADVANCED_FACE ( 'NONE', ( #11930 ), #5850, .T. ) ;
#18058=VERTEX_POINT ( 'NONE', #7105 ) ;
#18064=CARTESIAN_POINT ( 'NONE',  ( 0.000000000000000000, 147.7545334744432921, 496.6642397995874489 ) ) ;
#18065=LINE ( 'NONE', #3966, #16638 ) ;
#18075=AXIS2_PLACEMENT_3D ( 'NONE', #15427, #18302, #1255 ) ;
#18082=DIRECTION ( 'NONE',  ( 0.000000000000000000, -0.7071067811865475727, -0.7071067811865475727 ) ) ;
#18086=CIRCLE ( 'NONE', #6938, 1.000000000000004219 ) ;
#18090=CARTESIAN_POINT ( 'NONE',  ( -0.7456292300257998384, 138.9173202923915653, 489.3604919264676596 ) ) ;
#18117=EDGE_CURVE ( 'NONE', #12429, #14767, #12043, .T. ) ;
#18132=EDGE_CURVE ( 'NONE', #3908, #4572, #4297, .T. ) ;
#18133=CARTESIAN_POINT ( 'NONE',  ( -81.18192946989245229, 147.7545334744432921, 491.0690926367356042 ) ) ;
#18136=FILL_AREA_STYLE_COLOUR ( '', #2044 ) ;
#18149=MECHANICAL_DESIGN_GEOMETRIC_PRESENTATION_REPRESENTATION('',(#9594),#3024);
#18150=ORIENTED_EDGE ( 'NONE', *, *, #3726, .F. ) ;
#18155=ORIENTED_EDGE ( 'NONE', *, *, #8431, .T. ) ;
#18157=CARTESIAN_POINT ( 'NONE',  ( -79.38291287507639993, 139.9432517092814692, 501.1364486412747397 ) ) ;
#18158=FACE_OUTER_BOUND ( 'NONE', #13756, .T. ) ;
#18161=DIRECTION ( 'NONE',  ( 0.000000000000000000, 0.000000000000000000, -1.000000000000000000 ) ) ;
#18166=( GEOMETRIC_REPRESENTATION_CONTEXT ( 3 ) GLOBAL_UNCERTAINTY_ASSIGNED_CONTEXT ( ( #7042 ) ) GLOBAL_UNIT_ASSIGNED_CONTEXT ( ( #15339, #5944, #13398 ) ) REPRESENTATION_CONTEXT ( 'NONE', 'WORKASPACE' ) );
#18172=ORIENTED_EDGE ( 'NONE', *, *, #1852, .F. ) ;
#18176=AXIS2_PLACEMENT_3D ( 'NONE', #14168, #12435, #15646 ) ;
#18177=ADVANCED_FACE ( 'NONE', ( #15431 ), #14278, .T. ) ;
#18192=CARTESIAN_POINT ( 'NONE',  ( -1.301042606982605321E-14, 139.2066006846527841, 488.2525619656396429 ) ) ;
#18197=FILL_AREA_STYLE_COLOUR ( '', #66 ) ;
#18215=( NAMED_UNIT ( * ) SI_UNIT ( $, .STERADIAN. ) SOLID_ANGLE_UNIT ( ) );
#18219=CYLINDRICAL_SURFACE ( 'NONE', #7876, 1.000000000000000888 ) ;
#18222=CIRCLE ( 'NONE', #13006, 8.000000000000007105 ) ;
#18234=( GEOMETRIC_REPRESENTATION_CONTEXT ( 3 ) GLOBAL_UNCERTAINTY_ASSIGNED_CONTEXT ( ( #19376 ) ) GLOBAL_UNIT_ASSIGNED_CONTEXT ( ( #19048, #2990, #6509 ) ) REPRESENTATION_CONTEXT ( 'NONE', 'WORKASPACE' ) );
#18236=VECTOR ( 'NONE', #3209, 1000.000000000000000 ) ;
#18240=VECTOR ( 'NONE', #16522, 1000.000000000000000 ) ;
#18247=DIRECTION ( 'NONE',  ( -0.000000000000000000, -1.000000000000000000, -0.000000000000000000 ) ) ;
#18249=CARTESIAN_POINT ( 'NONE',  ( -1.387778780781445676E-14, 216.7545334744432921, 500.8237260975782874 ) ) ;
#18250=FACE_OUTER_BOUND ( 'NONE', #4987, .T. ) ;
#18258=ORIENTED_EDGE ( 'NONE', *, *, #9245, .F. ) ;
#18268=VERTEX_POINT ( 'NONE', #12855 ) ;
#18273=CARTESIAN_POINT ( 'NONE',  ( -79.85426141749488238, 139.6565686763037206, 500.5947571826810076 ) ) ;
#18291=AXIS2_PLACEMENT_3D ( 'NONE', #18846, #4756, #8251 ) ;
#18297=ORIENTED_EDGE ( 'NONE', *, *, #10232, .F. ) ;
#18300=SURFACE_STYLE_FILL_AREA ( #10376 ) ;
#18302=DIRECTION ( 'NONE',  ( 0.000000000000000000, -1.000000000000000000, 0.000000000000000000 ) ) ;
#18306=DIRECTION ( 'NONE',  ( 0.000000000000000000, -1.000000000000000000, 0.000000000000000000 ) ) ;
#18309=CARTESIAN_POINT ( 'NONE',  ( -82.18192946989275072, 138.7545334744432637, 499.8237260975782306 ) ) ;
#18312=ORIENTED_EDGE ( 'NONE', *, *, #11262, .F. ) ;
#18329=ADVANCED_FACE ( 'NONE', ( #4763 ), #12702, .T. ) ;
#18338=VERTEX_POINT ( 'NONE', #14123 ) ;
#18342=UNCERTAINTY_MEASURE_WITH_UNIT (LENGTH_MEASURE( 1.000000000000000082E-05 ), #18048, 'distance_accuracy_value', 'NONE');
#18345=DIRECTION ( 'NONE',  ( -8.673617379884027583E-16, 0.000000000000000000, -1.000000000000000000 ) ) ;
#18347=EDGE_CURVE ( 'NONE', #10821, #14143, #15012, .T. ) ;
#18349=CARTESIAN_POINT ( 'NONE',  ( -79.99999999999995737, 216.7545334744432921, 510.3921618609452935 ) ) ;
#18352=ORIENTED_EDGE ( 'NONE', *, *, #17250, .F. ) ;
#18363=FACE_OUTER_BOUND ( 'NONE', #3368, .T. ) ;
#18368=CARTESIAN_POINT ( 'NONE',  ( -80.37285363047544706, 140.5927919537299715, 501.0285821077172841 ) ) ;
#18369=SURFACE_STYLE_FILL_AREA ( #15303 ) ;
#18372=DIRECTION ( 'NONE',  ( 0.000000000000000000, 1.000000000000000000, -0.000000000000000000 ) ) ;
#18375=EDGE_CURVE ( 'NONE', #12596, #1145, #11047, .T. ) ;
#18376=ORIENTED_EDGE ( 'NONE', *, *, #40, .T. ) ;
#18378=EDGE_LOOP ( 'NONE', ( #18150, #17471, #14933, #12162 ) ) ;
#18383=DIRECTION ( 'NONE',  ( -0.000000000000000000, -0.000000000000000000, 1.000000000000000000 ) ) ;
#18394=CIRCLE ( 'NONE', #931, 1.000000000000000888 ) ;
#18401=PRESENTATION_STYLE_ASSIGNMENT (( #20039 ) ) ;
#18411=VERTEX_POINT ( 'NONE', #14340 ) ;
#18419=SURFACE_SIDE_STYLE ('',( #2556 ) ) ;
#18430=ORIENTED_EDGE ( 'NONE', *, *, #3308, .F. ) ;
#18442=DIRECTION ( 'NONE',  ( 1.000000000000000000, 0.000000000000000000, 0.000000000000000000 ) ) ;
#18455=AXIS2_PLACEMENT_3D ( 'NONE', #19027, #14104, #9616 ) ;
#18465=CARTESIAN_POINT ( 'NONE',  ( -79.14393569841020337, 140.2407135942496268, 501.6205206800881342 ) ) ;
#18472=DIRECTION ( 'NONE',  ( 7.719519468096785259E-14, 0.000000000000000000, 1.000000000000000000 ) ) ;
#18477=EDGE_LOOP ( 'NONE', ( #7573, #4800, #12886, #14440 ) ) ;
#18478=DIRECTION ( 'NONE',  ( 0.000000000000000000, 0.000000000000000000, 1.000000000000000000 ) ) ;
#18480=AXIS2_PLACEMENT_3D ( 'NONE', #9514, #18782, #37 ) ;
#18481=ORIENTED_EDGE ( 'NONE', *, *, #16724, .F. ) ;
#18484=CARTESIAN_POINT ( 'NONE',  ( -81.00000000000127898, 216.7545334744432921, 489.5655098179835818 ) ) ;
#18486=CARTESIAN_POINT ( 'NONE',  ( -79.99999999999995737, 216.7545334744432921, 205.1946179577815883 ) ) ;
#18495=CARTESIAN_POINT ( 'NONE',  ( -58.16843972078500258, 319.7545334744432353, 485.1700099148404206 ) ) ;
#18502=TOROIDAL_SURFACE ( 'NONE', #15902, 8.000000000000000000, 1.000000000000000000 ) ;
#18514=DIRECTION ( 'NONE',  ( -0.000000000000000000, -1.000000000000000000, -0.000000000000000000 ) ) ;
#18517=COLOUR_RGB ( '', 0.31764706, 0.68627451, 0.89019608) ;
#18523=SURFACE_SIDE_STYLE ('',( #5781 ) ) ;
#18540=CYLINDRICAL_SURFACE ( 'NONE', #6454, 9.000000000000007105 ) ;
#18547=EDGE_CURVE ( 'NONE', #16123, #10884, #14252, .T. ) ;
#18548=AXIS2_PLACEMENT_3D ( 'NONE', #1844, #8154, #17209 ) ;
#18562=VECTOR ( 'NONE', #17032, 1000.000000000000000 ) ;
#18569=ORIENTED_EDGE ( 'NONE', *, *, #6559, .T. ) ;
#18570=CIRCLE ( 'NONE', #16320, 3.000000000000002665 ) ;
#18594=ORIENTED_EDGE ( 'NONE', *, *, #15797, .T. ) ;
#18595=PRESENTATION_STYLE_ASSIGNMENT (( #9608 ) ) ;
#18600=ORIENTED_EDGE ( 'NONE', *, *, #15707, .T. ) ;
#18622=CARTESIAN_POINT ( 'NONE',  ( 0.4333752514400535105, 138.7761994944360424, 490.4323031634212953 ) ) ;
#18630=CARTESIAN_POINT ( 'NONE',  ( -80.85741104738939100, 138.7723821175181627, 490.5025619656437357 ) ) ;
#18643=DIRECTION ( 'NONE',  ( -0.000000000000000000, -1.000000000000000000, -0.000000000000000000 ) ) ;
#18650=PRESENTATION_STYLE_ASSIGNMENT (( #17204 ) ) ;
#18678=DIRECTION ( 'NONE',  ( 7.714700791774628163E-14, 0.000000000000000000, 1.000000000000000000 ) ) ;
#18681=VECTOR ( 'NONE', #7294, 1000.000000000000000 ) ;
#18684=ADVANCED_FACE ( 'NONE', ( #14485 ), #8345, .T. ) ;
#18685=FILL_AREA_STYLE_COLOUR ( '', #9682 ) ;
#18686=VERTEX_POINT ( 'NONE', #17374 ) ;
#18688=DIRECTION ( 'NONE',  ( 0.000000000000000000, 1.000000000000000000, 0.000000000000000000 ) ) ;
#18692=ORIENTED_EDGE ( 'NONE', *, *, #19443, .F. ) ;
#18697=CARTESIAN_POINT ( 'NONE',  ( 0.3830880647780208204, 140.5989314160965762, 501.0334628959610654 ) ) ;
#18716=VERTEX_POINT ( 'NONE', #9337 ) ;
#18720=CARTESIAN_POINT ( 'NONE',  ( -80.44547052777866725, 138.7779086090105523, 490.4200269341494050 ) ) ;
#18728=CARTESIAN_POINT ( 'NONE',  ( -81.18192946989245229, 139.7545334744432637, 491.0690926367356042 ) ) ;
#18735=DIRECTION ( 'NONE',  ( 1.445602896647338128E-15, 0.000000000000000000, 1.000000000000000000 ) ) ;
#18740=ORIENTED_EDGE ( 'NONE', *, *, #17711, .T. ) ;
#18742=ORIENTED_EDGE ( 'NONE', *, *, #16803, .T. ) ;
#18750=VECTOR ( 'NONE', #9869, 1000.000000000000000 ) ;
#18753=CARTESIAN_POINT ( 'NONE',  ( 0.000000000000000000, 138.7545334744432637, 487.3411705753777596 ) ) ;
#18755=CARTESIAN_POINT ( 'NONE',  ( -79.99999999999995737, 216.7545334744432921, 515.1946179577817020 ) ) ;
#18772=AXIS2_PLACEMENT_3D ( 'NONE', #7369, #11809, #15307 ) ;
#18773=CARTESIAN_POINT ( 'NONE',  ( 0.1220691512310314308, 140.0123732041122935, 501.2786137957034498 ) ) ;
#18782=DIRECTION ( 'NONE',  ( -1.000000000000000000, 0.000000000000000000, 1.450371633464475582E-15 ) ) ;
#18783=ORIENTED_EDGE ( 'NONE', *, *, #1537, .T. ) ;
#18785=ORIENTED_EDGE ( 'NONE', *, *, #13493, .T. ) ;
#18807=EDGE_CURVE ( 'NONE', #14814, #9566, #5018, .T. ) ;
#18808=EDGE_CURVE ( 'NONE', #7676, #15757, #5062, .T. ) ;
#18810=VERTEX_POINT ( 'NONE', #3477 ) ;
#18812=CARTESIAN_POINT ( 'NONE',  ( -81.00000000000133582, 139.4861549369088323, 500.2186618848270996 ) ) ;
#18816=PLANE ( 'NONE',  #2054 ) ;
#18819=DIRECTION ( 'NONE',  ( -1.000000000000000000, 0.000000000000000000, -5.551115123125777653E-14 ) ) ;
#18828=CARTESIAN_POINT ( 'NONE',  ( -1.000000000000015543, 147.7545334744432921, 491.0690926367356042 ) ) ;
#18837=PLANE ( 'NONE',  #12009 ) ;
#18842=EDGE_CURVE ( 'NONE', #4572, #12596, #3573, .T. ) ;
#18843=CARTESIAN_POINT ( 'NONE',  ( -79.99999999999995737, 216.7545334744432921, 489.5655098179848892 ) ) ;
#18846=CARTESIAN_POINT ( 'NONE',  ( 0.000000000000000000, 138.7545334744432637, 0.000000000000000000 ) ) ;
#18850=SURFACE_STYLE_FILL_AREA ( #9177 ) ;
#18863=VECTOR ( 'NONE', #15585, 1000.000000000000000 ) ;
#18864=ORIENTED_EDGE ( 'NONE', *, *, #4771, .T. ) ;
#18868=CARTESIAN_POINT ( 'NONE',  ( -81.18192946989275072, 138.7545334744432637, 500.8237260975782874 ) ) ;
#18873=CARTESIAN_POINT ( 'NONE',  ( 0.2960399808010766298, 139.5465514659026667, 500.3567029293851647 ) ) ;
#18874=CARTESIAN_POINT ( 'NONE',  ( -41.50085094405407915, 159.0821755739672483, 505.3921618609452935 ) ) ;
#18889=ORIENTED_EDGE ( 'NONE', *, *, #15809, .F. ) ;
#18897=ORIENTED_EDGE ( 'NONE', *, *, #17469, .T. ) ;
#18920=ORIENTED_EDGE ( 'NONE', *, *, #16533, .T. ) ;
#18921=AXIS2_PLACEMENT_3D ( 'NONE', #13860, #1155, #5928 ) ;
#18925=CARTESIAN_POINT ( 'NONE',  ( -80.17963259596821501, 139.9670406124139674, 501.2044833972698825 ) ) ;
#18932=VECTOR ( 'NONE', #228, 1000.000000000000000 ) ;
#18937=DIRECTION ( 'NONE',  ( 1.000000000000000000, 0.000000000000000000, 0.000000000000000000 ) ) ;
#18948=ORIENTED_EDGE ( 'NONE', *, *, #9618, .F. ) ;
#18954=FACE_OUTER_BOUND ( 'NONE', #12445, .T. ) ;
#18973=LINE ( 'NONE', #24, #4432 ) ;
#18975=CARTESIAN_POINT ( 'NONE',  ( -0.1029799530868260177, 140.5738215973348701, 502.0971144060484335 ) ) ;
#18997=CARTESIAN_POINT ( 'NONE',  ( -81.00000000000127898, 139.7703989349477354, 489.5655098179835818 ) ) ;
#19027=CARTESIAN_POINT ( 'NONE',  ( -81.18192946989242387, 139.7703989349477354, 490.5655098180907885 ) ) ;
#19030=ORIENTED_EDGE ( 'NONE', *, *, #5218, .T. ) ;
#19033=AXIS2_PLACEMENT_3D ( 'NONE', #11837, #968, #3696 ) ;
#19036=VERTEX_POINT ( 'NONE', #15308 ) ;
#19039=CARTESIAN_POINT ( 'NONE',  ( -79.99999999999995737, 316.7545334744432353, 495.1946179577816451 ) ) ;
#19040=( LENGTH_UNIT ( ) NAMED_UNIT ( * ) SI_UNIT ( .MILLI., .METRE. ) );
#19048=( LENGTH_UNIT ( ) NAMED_UNIT ( * ) SI_UNIT ( .MILLI., .METRE. ) );
#19070=DIRECTION ( 'NONE',  ( -0.000000000000000000, -0.7071067811865614505, -0.7071067811865336949 ) ) ;
#19074=DIRECTION ( 'NONE',  ( 0.000000000000000000, 0.7071067811865336949, -0.7071067811865614505 ) ) ;
#19075=CARTESIAN_POINT ( 'NONE',  ( -1.214306433183764808E-14, 140.8764026050585301, 502.4686618848270996 ) ) ;
#19077=CARTESIAN_POINT ( 'NONE',  ( -79.99999999999995737, 140.1563709946295262, 488.5655098179835818 ) ) ;
#19090=VERTEX_POINT ( 'NONE', #12827 ) ;
#19093=DIRECTION ( 'NONE',  ( 0.000000000000000000, 0.000000000000000000, 1.000000000000000000 ) ) ;
#19094=B_SPLINE_CURVE_WITH_KNOTS ( 'NONE', 3,
 ( #452, #12953, #350, #5116, #9741, #17672, #3561, #5213, #14773, #16253 ),
 .UNSPECIFIED., .F., .F.,
 ( 4, 2, 2, 2, 4 ),
 ( 0.000000000000000000, 0.0004090546821513940776, 0.0008181093643027881552, 0.001227164046454182287, 0.001636218728605576310 ),
 .UNSPECIFIED. ) ;
#19095=ADVANCED_FACE ( 'NONE', ( #1558 ), #12419, .F. ) ;
#19100=ADVANCED_FACE ( 'NONE', ( #5203 ), #13236, .F. ) ;
#19108=DIRECTION ( 'NONE',  ( 0.000000000000000000, 0.000000000000000000, -1.000000000000000000 ) ) ;
#19110=ORIENTED_EDGE ( 'NONE', *, *, #8631, .T. ) ;
#19116=CYLINDRICAL_SURFACE ( 'NONE', #12911, 3.000000000000016431 ) ;
#19125=VERTEX_POINT ( 'NONE', #11474 ) ;
#19126=CARTESIAN_POINT ( 'NONE',  ( -80.31210361190693447, 139.8880426697628820, 501.0724697727050057 ) ) ;
#19132=CARTESIAN_POINT ( 'NONE',  ( -1.274252908074454287E-14, 140.1563709946295262, 488.5655098179835818 ) ) ;
#19143=CIRCLE ( 'NONE', #6339, 9.000000000000007105 ) ;
#19144=VERTEX_POINT ( 'NONE', #14675 ) ;
#19157=DIRECTION ( 'NONE',  ( 0.000000000000000000, 0.7071067811865504593, -0.7071067811865445751 ) ) ;
#19169=CARTESIAN_POINT ( 'NONE',  ( 2.181929469892510465, 139.7703989349544145, 490.5655098179848324 ) ) ;
#19174=VECTOR ( 'NONE', #14083, 1000.000000000000000 ) ;
#19179=VERTEX_POINT ( 'NONE', #14559 ) ;
#19185=CARTESIAN_POINT ( 'NONE',  ( -1.000000000000009104, 142.0976792249509231, 485.4122383872432351 ) ) ;
#19199=VECTOR ( 'NONE', #4754, 1000.000000000000000 ) ;
#19200=ORIENTED_EDGE ( 'NONE', *, *, #11630, .T. ) ;
#19204=EDGE_LOOP ( 'NONE', ( #648, #9295, #16096 ) ) ;
#19209=DIRECTION ( 'NONE',  ( 0.000000000000000000, 0.000000000000000000, 1.000000000000000000 ) ) ;
#19221=SURFACE_SIDE_STYLE ('',( #1986 ) ) ;
#19235=EDGE_LOOP ( 'NONE', ( #8553, #9614, #1241, #13995, #8226, #14294 ) ) ;
#19248=AXIS2_PLACEMENT_3D ( 'NONE', #3636, #5286, #622 ) ;
#19262=CIRCLE ( 'NONE', #3804, 7.999999999999952038 ) ;
#19275=CARTESIAN_POINT ( 'NONE',  ( -79.99999999999995737, 216.7545334744432921, 510.3921618609452935 ) ) ;
#19300=DIRECTION ( 'NONE',  ( 0.000000000000000000, 0.000000000000000000, 1.000000000000000000 ) ) ;
#19307=AXIS2_PLACEMENT_3D ( 'NONE', #3888, #5631, #6797 ) ;
#19316=CYLINDRICAL_SURFACE ( 'NONE', #14771, 8.999999999999952038 ) ;
#19320=SURFACE_SIDE_STYLE ('',( #17778 ) ) ;
#19338=CARTESIAN_POINT ( 'NONE',  ( -79.99999999999995737, 216.7545334744432921, 512.1946179577817020 ) ) ;
#19340=CARTESIAN_POINT ( 'NONE',  ( 0.1987446979796453350, 139.8600507635789825, 489.1673953262136934 ) ) ;
#19341=DIRECTION ( 'NONE',  ( 0.000000000000000000, 0.000000000000000000, 1.000000000000000000 ) ) ;
#19348=ORIENTED_EDGE ( 'NONE', *, *, #18132, .T. ) ;
#19355=EDGE_CURVE ( 'NONE', #10076, #19819, #1631, .T. ) ;
#19358=DIRECTION ( 'NONE',  ( 1.000000000000000000, 0.000000000000000000, 0.000000000000000000 ) ) ;
#19367=CIRCLE ( 'NONE', #18044, 0.9999999999999995559 ) ;
#19368=VERTEX_POINT ( 'NONE', #14230 ) ;
#19375=ORIENTED_EDGE ( 'NONE', *, *, #1036, .T. ) ;
#19376=UNCERTAINTY_MEASURE_WITH_UNIT (LENGTH_MEASURE( 1.000000000000000082E-05 ), #19048, 'distance_accuracy_value', 'NONE');
#19385=CARTESIAN_POINT ( 'NONE',  ( -79.99999999999995737, 140.1563709946295262, 488.5655098179835818 ) ) ;
#19393=DIRECTION ( 'NONE',  ( 0.000000000000000000, 0.000000000000000000, -1.000000000000000000 ) ) ;
#19432=EDGE_CURVE ( 'NONE', #2723, #14489, #3420, .T. ) ;
#19433=FACE_OUTER_BOUND ( 'NONE', #4947, .T. ) ;
#19443=EDGE_CURVE ( 'NONE', #19903, #8271, #13123, .T. ) ;
#19447=ORIENTED_EDGE ( 'NONE', *, *, #1635, .T. ) ;
#19451=CARTESIAN_POINT ( 'NONE',  ( 0.9999999999999876765, 138.7545334744432637, 501.8237260975781737 ) ) ;
#19452=EDGE_CURVE ( 'NONE', #3836, #4888, #16321, .T. ) ;
#19453=SPHERICAL_SURFACE ( 'NONE', #6254, 1.000000000000000000 ) ;
#19454=DIRECTION ( 'NONE',  ( -0.000000000000000000, -1.000000000000000000, -0.000000000000000000 ) ) ;
#19459=EDGE_CURVE ( 'NONE', #17220, #16810, #9701, .T. ) ;
#19461=VECTOR ( 'NONE', #19733, 1000.000000000000000 ) ;
#19462=ORIENTED_EDGE ( 'NONE', *, *, #17179, .F. ) ;
#19473=DIRECTION ( 'NONE',  ( 0.000000000000000000, 0.000000000000000000, -1.000000000000000000 ) ) ;
#19487=VECTOR ( 'NONE', #10890, 1000.000000000000114 ) ;
#19489=VERTEX_POINT ( 'NONE', #19169 ) ;
#19522=LINE ( 'NONE', #6987, #15558 ) ;
#19530=DIRECTION ( 'NONE',  ( 0.000000000000000000, 1.000000000000000000, 0.000000000000000000 ) ) ;
#19537=EDGE_LOOP ( 'NONE', ( #13964, #18889, #7643, #14239 ) ) ;
#19548=VECTOR ( 'NONE', #16414, 1000.000000000000000 ) ;
#19553=VECTOR ( 'NONE', #6312, 1000.000000000000000 ) ;
#19557=( LENGTH_UNIT ( ) NAMED_UNIT ( * ) SI_UNIT ( .MILLI., .METRE. ) );
#19558=STYLED_ITEM ( 'NONE', ( #14946 ), #2057 ) ;
#19559=SURFACE_STYLE_USAGE ( .BOTH. , #13310 ) ;
#19563=EDGE_CURVE ( 'NONE', #17153, #5319, #14744, .T. ) ;
#19564=CARTESIAN_POINT ( 'NONE',  ( -79.96195573192551365, 139.0956700764377558, 488.6001242439256202 ) ) ;
#19575=DIRECTION ( 'NONE',  ( 1.000000000000000000, -0.000000000000000000, -1.450371633464475582E-15 ) ) ;
#19576=UNCERTAINTY_MEASURE_WITH_UNIT (LENGTH_MEASURE( 1.000000000000000082E-05 ), #3802, 'distance_accuracy_value', 'NONE');
#19579=EDGE_CURVE ( 'NONE', #4262, #3611, #16214, .T. ) ;
#19582=ORIENTED_EDGE ( 'NONE', *, *, #14565, .T. ) ;
#19588=CARTESIAN_POINT ( 'NONE',  ( -80.33275375302500265, 138.8974262895977745, 489.3169310699432231 ) ) ;
#19591=CARTESIAN_POINT ( 'NONE',  ( -80.99999999999995737, 140.4048636633015406, 500.8237260975782874 ) ) ;
#19594=ORIENTED_EDGE ( 'NONE', *, *, #6217, .T. ) ;
#19599=EDGE_LOOP ( 'NONE', ( #13067, #341, #4464, #7014 ) ) ;
#19605=CARTESIAN_POINT ( 'NONE',  ( -79.99999999999995737, 316.7545334744432353, 515.1946179577817020 ) ) ;
#19606=DIRECTION ( 'NONE',  ( 0.000000000000000000, 0.000000000000000000, -1.000000000000000000 ) ) ;
#19607=DIRECTION ( 'NONE',  ( 7.715811803773179210E-14, 0.000000000000000000, 1.000000000000000000 ) ) ;
#19610=DIRECTION ( 'NONE',  ( -0.000000000000000000, -0.000000000000000000, 1.000000000000000000 ) ) ;
#19641=ORIENTED_EDGE ( 'NONE', *, *, #4607, .F. ) ;
#19642=ORIENTED_EDGE ( 'NONE', *, *, #19443, .T. ) ;
#19655=DIRECTION ( 'NONE',  ( -0.000000000000000000, 1.000000000000000000, -0.000000000000000000 ) ) ;
#19660=EDGE_CURVE ( 'NONE', #5074, #19976, #821, .T. ) ;
#19672=EDGE_CURVE ( 'NONE', #9566, #8826, #2455, .T. ) ;
#19688=VECTOR ( 'NONE', #7644, 1000.000000000000000 ) ;
#19694=FACE_OUTER_BOUND ( 'NONE', #13607, .T. ) ;
#19699=CARTESIAN_POINT ( 'NONE',  ( -78.99999999999995737, 142.0976792249508946, 485.4122383872432351 ) ) ;
#19701=DIRECTION ( 'NONE',  ( 0.000000000000000000, 0.000000000000000000, 1.000000000000000000 ) ) ;
#19708=ORIENTED_EDGE ( 'NONE', *, *, #16807, .F. ) ;
#19712=EDGE_CURVE ( 'NONE', #15985, #18686, #14165, .T. ) ;
#19713=VERTEX_POINT ( 'NONE', #1763 ) ;
#19725=CARTESIAN_POINT ( 'NONE',  ( 0.2407302285477639081, 139.8437824378728180, 489.2196001188304990 ) ) ;
#19733=DIRECTION ( 'NONE',  ( -0.000000000000000000, -1.000000000000000000, -0.000000000000000000 ) ) ;
#19734=CARTESIAN_POINT ( 'NONE',  ( 0.9999999999999876765, 216.7545334744432921, 501.8237260975781737 ) ) ;
#19744=ORIENTED_EDGE ( 'NONE', *, *, #12487, .F. ) ;
#19757=CARTESIAN_POINT ( 'NONE',  ( -79.99999999999995737, 140.0740644222055948, 488.6904065690556536 ) ) ;
#19768=ORIENTED_EDGE ( 'NONE', *, *, #10655, .T. ) ;
#19772=DIRECTION ( 'NONE',  ( -0.000000000000000000, 1.000000000000000000, -0.000000000000000000 ) ) ;
#19776=DIRECTION ( 'NONE',  ( 0.000000000000000000, 1.000000000000000000, 0.000000000000000000 ) ) ;
#19781=CARTESIAN_POINT ( 'NONE',  ( -81.00000000000136424, 138.8314847490560169, 489.5655098179835818 ) ) ;
#19789=EDGE_LOOP ( 'NONE', ( #6496, #20326, #13451, #13359 ) ) ;
#19799=CARTESIAN_POINT ( 'NONE',  ( -1.274252908074454287E-14, 216.7545334744432921, 488.5655098179835818 ) ) ;
#19805=ORIENTED_EDGE ( 'NONE', *, *, #17179, .T. ) ;
#19806=FACE_OUTER_BOUND ( 'NONE', #6341, .T. ) ;
#19819=VERTEX_POINT ( 'NONE', #14454 ) ;
#19825=AXIS2_PLACEMENT_3D ( 'NONE', #15792, #7641, #7944 ) ;
#19827=ADVANCED_FACE ( 'NONE', ( #8284 ), #14553, .T. ) ;
#19830=LINE ( 'NONE', #4097, #11603 ) ;
#19846=EDGE_LOOP ( 'NONE', ( #10052, #9531, #3358, #4000 ) ) ;
#19848=VECTOR ( 'NONE', #1790, 1000.000000000000000 ) ;
#19865=DIRECTION ( 'NONE',  ( 0.000000000000000000, -0.7071067811865614505, -0.7071067811865336949 ) ) ;
#19868=CARTESIAN_POINT ( 'NONE',  ( -38.50085094405407204, 209.4098724938429541, 505.3921618609452935 ) ) ;
#19873=VECTOR ( 'NONE', #11237, 1000.000000000000000 ) ;
#19879=CARTESIAN_POINT ( 'NONE',  ( -64.99999999999995737, 317.7545334744432353, 495.1946179577816451 ) ) ;
#19887=DIRECTION ( 'NONE',  ( 0.000000000000000000, -0.000000000000000000, 1.000000000000000000 ) ) ;
#19888=CIRCLE ( 'NONE', #12331, 1.000000000000001110 ) ;
#19903=VERTEX_POINT ( 'NONE', #5687 ) ;
#19906=ORIENTED_EDGE ( 'NONE', *, *, #13931, .T. ) ;
#19912=EDGE_CURVE ( 'NONE', #3170, #17380, #10219, .T. ) ;
#19915=DIRECTION ( 'NONE',  ( -1.000000000000000000, 0.000000000000000000, 7.715811803773179210E-14 ) ) ;
#19916=CYLINDRICAL_SURFACE ( 'NONE', #18772, 1.000000000000015987 ) ;
#19933=DIRECTION ( 'NONE',  ( 5.540106248408141539E-14, 0.06294785233063035501, -0.9980168174369414835 ) ) ;
#19936=CARTESIAN_POINT ( 'NONE',  ( -79.99999999999995737, 316.7545334744432353, 495.1946179577816451 ) ) ;
#19940=CARTESIAN_POINT ( 'NONE',  ( -78.99999999999995737, 147.7545334744432921, 491.0690926367356042 ) ) ;
#19941=SURFACE_STYLE_FILL_AREA ( #11932 ) ;
#19958=VERTEX_POINT ( 'NONE', #15169 ) ;
#19962=PLANE ( 'NONE',  #1742 ) ;
#19964=CARTESIAN_POINT ( 'NONE',  ( -79.99999999999995737, 0.000000000000000000, 0.000000000000000000 ) ) ;
#19966=CARTESIAN_POINT ( 'NONE',  ( -81.18192946989275072, 216.7545334744432921, 499.8237260975782874 ) ) ;
#19974=ADVANCED_FACE ( 'NONE', ( #10531 ), #5506, .T. ) ;
#19976=VERTEX_POINT ( 'NONE', #4986 ) ;
#19984=CARTESIAN_POINT ( 'NONE',  ( 0.000000000000000000, 138.7723821175183048, 490.5025619656410640 ) ) ;
#19991=CARTESIAN_POINT ( 'NONE',  ( -79.76822305802286905, 138.8141600818972847, 490.0314170930259934 ) ) ;
#20000=CARTESIAN_POINT ( 'NONE',  ( -78.99999999999995737, 141.3905724437643414, 503.0282008302663144 ) ) ;
#20005=CARTESIAN_POINT ( 'NONE',  ( -80.65880741189570813, 140.4539905958026509, 500.8798623167376718 ) ) ;
#20015=VERTEX_POINT ( 'NONE', #331 ) ;
#20020=DIRECTION ( 'NONE',  ( 0.000000000000000000, 0.000000000000000000, 1.000000000000000000 ) ) ;
#20024=DIRECTION ( 'NONE',  ( 0.000000000000000000, 0.000000000000000000, 1.000000000000000000 ) ) ;
#20028=CIRCLE ( 'NONE', #17413, 1.000000000000000888 ) ;
#20035=PRESENTATION_STYLE_ASSIGNMENT (( #4208 ) ) ;
#20036=DIRECTION ( 'NONE',  ( 1.000000000000000000, 0.000000000000000000, 0.000000000000000000 ) ) ;
#20039=SURFACE_STYLE_USAGE ( .BOTH. , #12128 ) ;
#20047=AXIS2_PLACEMENT_3D ( 'NONE', #1134, #16539, #5509 ) ;
#20048=ORIENTED_EDGE ( 'NONE', *, *, #6885, .T. ) ;
#20058=ADVANCED_FACE ( 'NONE', ( #16038 ), #8080, .T. ) ;
#20065=LINE ( 'NONE', #817, #3654 ) ;
#20068=CARTESIAN_POINT ( 'NONE',  ( -81.18192946989275072, 140.4048636633015406, 500.8237260975782874 ) ) ;
#20074=ORIENTED_EDGE ( 'NONE', *, *, #13216, .T. ) ;
#20078=ORIENTED_EDGE ( 'NONE', *, *, #14393, .F. ) ;
#20084=LINE ( 'NONE', #19984, #12897 ) ;
#20089=PLANE ( 'NONE',  #15603 ) ;
#20095=CARTESIAN_POINT ( 'NONE',  ( -1.000000000000012657, 140.6767719171587316, 502.2321032788613593 ) ) ;
#20096=ORIENTED_EDGE ( 'NONE', *, *, #1682, .T. ) ;
#20103=ORIENTED_EDGE ( 'NONE', *, *, #15716, .F. ) ;
#20115=CARTESIAN_POINT ( 'NONE',  ( -80.82377052886815250, 140.4150287883843191, 500.8356803534629194 ) ) ;
#20116=DIRECTION ( 'NONE',  ( 0.000000000000000000, 0.000000000000000000, -1.000000000000000000 ) ) ;
#20119=LINE ( 'NONE', #17050, #9907 ) ;
#20127=ORIENTED_EDGE ( 'NONE', *, *, #15759, .F. ) ;
#20137=CARTESIAN_POINT ( 'NONE',  ( -79.99999999999995737, 152.4824555358010798, 501.3921618609452366 ) ) ;
#20150=AXIS2_PLACEMENT_3D ( 'NONE', #10127, #11677, #3541 ) ;
#20158=VERTEX_POINT ( 'NONE', #4422 ) ;
#20159=LINE ( 'NONE', #9057, #12656 ) ;
#20169=( LENGTH_UNIT ( ) NAMED_UNIT ( * ) SI_UNIT ( .MILLI., .METRE. ) );
#20185=EDGE_LOOP ( 'NONE', ( #17491, #12306, #4305, #11525 ) ) ;
#20193=PLANE ( 'NONE',  #3651 ) ;
#20197=CARTESIAN_POINT ( 'NONE',  ( 0.9999999999998859801, 139.7733885855926133, 500.8237260975781737 ) ) ;
#20209=ADVANCED_FACE ( 'NONE', ( #13600 ), #16800, .F. ) ;
#20225=DIRECTION ( 'NONE',  ( -0.000000000000000000, 1.000000000000000000, -0.000000000000000000 ) ) ;
#20226=DIRECTION ( 'NONE',  ( 0.000000000000000000, 0.000000000000000000, -1.000000000000000000 ) ) ;
#20231=ORIENTED_EDGE ( 'NONE', *, *, #2158, .T. ) ;
#20233=EDGE_LOOP ( 'NONE', ( #3658, #7967, #8221, #12861 ) ) ;
#20250=CARTESIAN_POINT ( 'NONE',  ( 0.9999999999998859801, 140.4048636633015406, 500.8237260975781737 ) ) ;
#20257=FACE_OUTER_BOUND ( 'NONE', #6040, .T. ) ;
#20265=CIRCLE ( 'NONE', #16674, 1.000000000000000888 ) ;
#20269=CARTESIAN_POINT ( 'NONE',  ( -79.08769456577726942, 139.0123798169321958, 488.9260675989677907 ) ) ;
#20277=CARTESIAN_POINT ( 'NONE',  ( -1.000000000000012434, 141.6406393683235194, 501.8237260975781737 ) ) ;
#20279=CARTESIAN_POINT ( 'NONE',  ( -44.50085094405410757, 209.4098724938429541, 505.3921618609452935 ) ) ;
#20280=CARTESIAN_POINT ( 'NONE',  ( -41.50085094405407915, 175.4489062796178871, 505.3921618609452935 ) ) ;
#20288=DIRECTION ( 'NONE',  ( -1.000000000000000000, 0.000000000000000000, -1.322948291343119651E-12 ) ) ;
#20290=ORIENTED_EDGE ( 'NONE', *, *, #15716, .T. ) ;
#20299=EDGE_CURVE ( 'NONE', #13854, #17453, #15773, .T. ) ;
#20304=ORIENTED_EDGE ( 'NONE', *, *, #14720, .F. ) ;
#20307=EDGE_CURVE ( 'NONE', #1465, #625, #9655, .T. ) ;
#20309=ORIENTED_EDGE ( 'NONE', *, *, #5012, .T. ) ;
#20319=FILL_AREA_STYLE_COLOUR ( '', #3124 ) ;
#20322=EDGE_CURVE ( 'NONE', #584, #16123, #3281, .T. ) ;
#20326=ORIENTED_EDGE ( 'NONE', *, *, #9494, .F. ) ;
#20331=DIRECTION ( 'NONE',  ( 2.775557561562888827E-14, 0.000000000000000000, -1.000000000000000000 ) ) ;
#20350=DIRECTION ( 'NONE',  ( -1.135258727068399668E-15, 0.000000000000000000, 1.000000000000000000 ) ) ;
#20361=CARTESIAN_POINT ( 'NONE',  ( -80.45802087912527156, 140.5471886258677614, 500.9805408940079019 ) ) ;
#20364=VECTOR ( 'NONE', #10837, 1000.000000000000000 ) ;
#20366=CIRCLE ( 'NONE', #11499, 1.000000000000000888 ) ;
#20370=CARTESIAN_POINT ( 'NONE',  ( 1.181929469892549101, 147.7545334744432921, 491.0690926367356042 ) ) ;
#20371=LINE ( 'NONE', #17088, #1747 ) ;
ENDSEC;
END-ISO-10303-21;
